ISO-10303-21;
HEADER;
FILE_DESCRIPTION (('STEP AP214'),
    '1' );
FILE_NAME ('3-Flange Yoke.step',
    '2026-10-28T16:50:19',
    ( '' ),
    ( '' ),
    'SwSTEP 2.0',
    'SolidWorks 2024',
    '' );
FILE_SCHEMA (( 'AUTOMOTIVE_DESIGN' ));
ENDSEC;

DATA;
#2=FACE_BOUND ( 'NONE', #8236, .T. ) ;
#6=EDGE_CURVE ( 'NONE', #2372, #8340, #1987, .T. ) ;
#9=ORIENTED_EDGE ( 'NONE', *, *, #306, .F. ) ;
#12=DIRECTION ( 'NONE',  ( 0.000000000000000000, 0.000000000000000000, -1.000000000000000000 ) ) ;
#14=CARTESIAN_POINT ( 'NONE',  ( 26.21170834203230982, 53.97171801779368394, -2.612255525622733554 ) ) ;
#16=LINE ( 'NONE', #2270, #110 ) ;
#18=VERTEX_POINT ( 'NONE', #6645 ) ;
#19=EDGE_CURVE ( 'NONE', #8372, #438, #65, .T. ) ;
#21=EDGE_CURVE ( 'NONE', #6915, #8464, #3515, .T. ) ;
#26=VECTOR ( 'NONE', #5373, 1000.000000000000000 ) ;
#30=ORIENTED_EDGE ( 'NONE', *, *, #4937, .F. ) ;
#36=( BOUNDED_CURVE ( )  B_SPLINE_CURVE ( 3, ( #9430, #2857, #1405, #8718 ),
 .UNSPECIFIED., .F., .F. ) 
 B_SPLINE_CURVE_WITH_KNOTS ( ( 4, 4 ),
 ( 0.6692669939101983934, 1.047197551196597853 ),
 .UNSPECIFIED. ) 
 CURVE ( )  GEOMETRIC_REPRESENTATION_ITEM ( )  RATIONAL_B_SPLINE_CURVE ( ( 1.000000000000000000, 0.9881327504826167285, 0.9881327504826167285, 1.000000000000000000 ) ) 
 REPRESENTATION_ITEM ( '' )  );
#37=EDGE_CURVE ( 'NONE', #4781, #2523, #3325, .T. ) ;
#41=LINE ( 'NONE', #8503, #1449 ) ;
#43=FACE_OUTER_BOUND ( 'NONE', #6081, .T. ) ;
#46=ORIENTED_EDGE ( 'NONE', *, *, #483, .F. ) ;
#47=CARTESIAN_POINT ( 'NONE',  ( -53.29490495164537833, 15.90990257669733943, -54.09009742330271564 ) ) ;
#48=VECTOR ( 'NONE', #5303, 999.9999999999998863 ) ;
#49=CARTESIAN_POINT ( 'NONE',  ( 34.25000000000000000, -43.00000000000000000, -25.00000000000000000 ) ) ;
#53=EDGE_LOOP ( 'NONE', ( #8094, #7825 ) ) ;
#55=VERTEX_POINT ( 'NONE', #1398 ) ;
#56=EDGE_CURVE ( 'NONE', #523, #4316, #9131, .T. ) ;
#58=DIRECTION ( 'NONE',  ( -1.000000000000000000, 0.000000000000000000, 0.000000000000000000 ) ) ;
#62=CARTESIAN_POINT ( 'NONE',  ( -53.29490495164537833, 15.90990257669733943, -85.90990257669729147 ) ) ;
#63=CARTESIAN_POINT ( 'NONE',  ( -53.29490495164537833, 15.90990257669733943, -51.09009742330271564 ) ) ;
#64=EDGE_LOOP ( 'NONE', ( #9455, #3764, #9081, #6496 ) ) ;
#65=LINE ( 'NONE', #2077, #6706 ) ;
#71=CARTESIAN_POINT ( 'NONE',  ( 53.29490495164537833, -30.00000000000000000, -97.50000000000002842 ) ) ;
#74=ORIENTED_EDGE ( 'NONE', *, *, #37, .F. ) ;
#75=VERTEX_POINT ( 'NONE', #1302 ) ;
#76=FACE_OUTER_BOUND ( 'NONE', #1771, .T. ) ;
#88=EDGE_LOOP ( 'NONE', ( #1645, #1926, #910, #5468 ) ) ;
#89=DIRECTION ( 'NONE',  ( 1.000000000000000000, -0.000000000000000000, -0.000000000000000000 ) ) ;
#95=VERTEX_POINT ( 'NONE', #8709 ) ;
#96=ORIENTED_EDGE ( 'NONE', *, *, #7565, .T. ) ;
#98=CARTESIAN_POINT ( 'NONE',  ( 37.00000000000000000, -30.00000000000000000, -95.00000000000000000 ) ) ;
#101=CARTESIAN_POINT ( 'NONE',  ( 0.000000000000000000, 0.000000000000000000, 11.99999999999999645 ) ) ;
#102=DIRECTION ( 'NONE',  ( -1.000000000000000000, 0.000000000000000000, 0.000000000000000000 ) ) ;
#103=DIRECTION ( 'NONE',  ( -0.000000000000000000, 0.7071067811865473507, 0.7071067811865477948 ) ) ;
#110=VECTOR ( 'NONE', #4520, 1000.000000000000000 ) ;
#116=CARTESIAN_POINT ( 'NONE',  ( 37.00000000000000000, -15.90990257669733943, -88.90990257669730568 ) ) ;
#121=EDGE_LOOP ( 'NONE', ( #3677, #5526, #8764, #3879, #8157 ) ) ;
#122=AXIS2_PLACEMENT_3D ( 'NONE', #7775, #7822, #1915 ) ;
#123=ORIENTED_EDGE ( 'NONE', *, *, #4714, .F. ) ;
#125=ADVANCED_FACE ( 'NONE', ( #5828 ), #4338, .F. ) ;
#127=CARTESIAN_POINT ( 'NONE',  ( 37.00000000000000000, 30.00000000000000000, -78.96446609406729067 ) ) ;
#128=DIRECTION ( 'NONE',  ( 0.000000000000000000, 0.000000000000000000, 1.000000000000000000 ) ) ;
#134=CYLINDRICAL_SURFACE ( 'NONE', #6817, 11.00000000000000000 ) ;
#135=EDGE_CURVE ( 'NONE', #3234, #301, #2169, .T. ) ;
#137=EDGE_CURVE ( 'NONE', #7845, #1132, #8358, .T. ) ;
#147=LINE ( 'NONE', #8971, #1968 ) ;
#149=FACE_BOUND ( 'NONE', #7075, .T. ) ;
#153=EDGE_CURVE ( 'NONE', #2399, #367, #4869, .T. ) ;
#156=EDGE_CURVE ( 'NONE', #7922, #4540, #818, .T. ) ;
#158=DIRECTION ( 'NONE',  ( 0.000000000000000000, 0.000000000000000000, -1.000000000000000000 ) ) ;
#160=CARTESIAN_POINT ( 'NONE',  ( 53.29490495164537833, 18.67545040036925386, -90.28901569369799063 ) ) ;
#162=AXIS2_PLACEMENT_3D ( 'NONE', #9418, #584, #3511 ) ;
#163=PLANE ( 'NONE',  #7256 ) ;
#172=ORIENTED_EDGE ( 'NONE', *, *, #9280, .F. ) ;
#174=ORIENTED_EDGE ( 'NONE', *, *, #2719, .T. ) ;
#175=CARTESIAN_POINT ( 'NONE',  ( -37.22467645238199196, 47.05659850664387278, 11.99999999999999645 ) ) ;
#179=DIRECTION ( 'NONE',  ( -1.000000000000000000, 0.000000000000000000, 0.000000000000000000 ) ) ;
#183=EDGE_LOOP ( 'NONE', ( #6953, #2067, #7066, #3737 ) ) ;
#188=EDGE_LOOP ( 'NONE', ( #6810, #8765 ) ) ;
#191=DIRECTION ( 'NONE',  ( 0.000000000000000000, 1.000000000000000000, 0.000000000000000000 ) ) ;
#196=AXIS2_PLACEMENT_3D ( 'NONE', #1778, #5349, #383 ) ;
#207=DIRECTION ( 'NONE',  ( 0.000000000000000000, 0.000000000000000000, 1.000000000000000000 ) ) ;
#211=EDGE_LOOP ( 'NONE', ( #5742, #6073, #5276, #6526 ) ) ;
#215=PLANE ( 'NONE',  #7192 ) ;
#216=ORIENTED_EDGE ( 'NONE', *, *, #5023, .T. ) ;
#220=ORIENTED_EDGE ( 'NONE', *, *, #19, .T. ) ;
#222=CARTESIAN_POINT ( 'NONE',  ( 38.00000000000000000, -43.00000000000000000, -7.366666666666667140 ) ) ;
#225=CARTESIAN_POINT ( 'NONE',  ( -53.29490495164537833, -3.673940397442057600E-15, -70.00000000000000000 ) ) ;
#228=EDGE_CURVE ( 'NONE', #3453, #8277, #1798, .T. ) ;
#231=EDGE_LOOP ( 'NONE', ( #8033, #1343, #3899, #2281 ) ) ;
#232=CARTESIAN_POINT ( 'NONE',  ( -60.00000000000000000, -30.00000000000000000, -30.00000000000000000 ) ) ;
#234=CARTESIAN_POINT ( 'NONE',  ( -38.00000000000000711, -43.00000000000000000, 11.99999999999999645 ) ) ;
#240=CARTESIAN_POINT ( 'NONE',  ( 37.00000000000000000, -30.00000000000000000, -95.00000000000000000 ) ) ;
#243=ORIENTED_EDGE ( 'NONE', *, *, #7351, .F. ) ;
#251=EDGE_CURVE ( 'NONE', #900, #5694, #9127, .T. ) ;
#253=ADVANCED_FACE ( 'NONE', ( #9175 ), #2610, .T. ) ;
#257=DIRECTION ( 'NONE',  ( -1.000000000000000000, 0.000000000000000000, 0.000000000000000000 ) ) ;
#258=EDGE_CURVE ( 'NONE', #4079, #5088, #663, .T. ) ;
#260=CARTESIAN_POINT ( 'NONE',  ( 60.00000000000000000, -30.00000000000000355, -82.50000000000001421 ) ) ;
#261=CARTESIAN_POINT ( 'NONE',  ( -37.00000000000000711, -15.90990257669733943, -88.90990257669730568 ) ) ;
#262=VECTOR ( 'NONE', #7846, 1000.000000000000000 ) ;
#264=ORIENTED_EDGE ( 'NONE', *, *, #9231, .T. ) ;
#279=CIRCLE ( 'NONE', #8252, 11.00000000000000711 ) ;
#287=VERTEX_POINT ( 'NONE', #5444 ) ;
#289=AXIS2_PLACEMENT_3D ( 'NONE', #5072, #4352, #128 ) ;
#290=CARTESIAN_POINT ( 'NONE',  ( 37.00000000000000000, -15.90990257669733943, -85.90990257669729147 ) ) ;
#295=VECTOR ( 'NONE', #2775, 1000.000000000000000 ) ;
#299=FACE_OUTER_BOUND ( 'NONE', #231, .T. ) ;
#301=VERTEX_POINT ( 'NONE', #6269 ) ;
#303=CARTESIAN_POINT ( 'NONE',  ( 0.000000000000000000, -30.00000000000000000, 0.000000000000000000 ) ) ;
#304=DIRECTION ( 'NONE',  ( -1.000000000000000000, -0.000000000000000000, -0.000000000000000000 ) ) ;
#305=LINE ( 'NONE', #9085, #4587 ) ;
#306=EDGE_CURVE ( 'NONE', #1076, #8284, #1106, .T. ) ;
#313=VERTEX_POINT ( 'NONE', #3493 ) ;
#314=CARTESIAN_POINT ( 'NONE',  ( -53.29490495164537833, -27.56180520566615044, -81.40266088840114378 ) ) ;
#317=DIRECTION ( 'NONE',  ( -0.000000000000000000, -0.000000000000000000, 1.000000000000000000 ) ) ;
#318=FACE_OUTER_BOUND ( 'NONE', #4303, .T. ) ;
#319=DIRECTION ( 'NONE',  ( 1.000000000000000000, -0.000000000000000000, -0.000000000000000000 ) ) ;
#324=ORIENTED_EDGE ( 'NONE', *, *, #657, .T. ) ;
#325=EDGE_CURVE ( 'NONE', #3453, #8519, #5765, .T. ) ;
#331=EDGE_CURVE ( 'NONE', #5110, #5683, #1782, .T. ) ;
#332=DIRECTION ( 'NONE',  ( 0.000000000000000000, 0.000000000000000000, 1.000000000000000000 ) ) ;
#335=ORIENTED_EDGE ( 'NONE', *, *, #1536, .T. ) ;
#337=CARTESIAN_POINT ( 'NONE',  ( -27.00000000000000000, -43.00000000000000000, 25.00000000000000000 ) ) ;
#345=CARTESIAN_POINT ( 'NONE',  ( 40.77961158827727672, -30.00000000000000000, -84.30964406271149869 ) ) ;
#349=EDGE_CURVE ( 'NONE', #1211, #8754, #4001, .T. ) ;
#350=AXIS2_PLACEMENT_3D ( 'NONE', #1501, #3715, #8755 ) ;
#353=ORIENTED_EDGE ( 'NONE', *, *, #5129, .F. ) ;
#356=DIRECTION ( 'NONE',  ( -1.000000000000000000, 0.000000000000000000, -0.000000000000000000 ) ) ;
#367=VERTEX_POINT ( 'NONE', #8420 ) ;
#368=EDGE_CURVE ( 'NONE', #6290, #8884, #8400, .T. ) ;
#369=CARTESIAN_POINT ( 'NONE',  ( 26.21170834203230982, -53.97171801779368394, -0.5000000000000038858 ) ) ;
#374=DIRECTION ( 'NONE',  ( 1.000000000000000000, -0.000000000000000000, -0.000000000000000000 ) ) ;
#383=DIRECTION ( 'NONE',  ( 1.000000000000000000, 0.000000000000000000, 0.000000000000000000 ) ) ;
#387=DIRECTION ( 'NONE',  ( -1.000000000000000000, 0.000000000000000000, 0.000000000000000000 ) ) ;
#394=ORIENTED_EDGE ( 'NONE', *, *, #228, .T. ) ;
#395=AXIS2_PLACEMENT_3D ( 'NONE', #3027, #5818, #6637 ) ;
#400=CARTESIAN_POINT ( 'NONE',  ( -27.00000000000000000, 43.00000000000000000, -25.00000000000000000 ) ) ;
#403=AXIS2_PLACEMENT_3D ( 'NONE', #1611, #2187, #4396 ) ;
#407=ADVANCED_FACE ( 'NONE', ( #6580 ), #3012, .F. ) ;
#409=DIRECTION ( 'NONE',  ( 0.000000000000000000, 0.000000000000000000, 1.000000000000000000 ) ) ;
#416=VECTOR ( 'NONE', #4660, 1000.000000000000114 ) ;
#423=ADVANCED_FACE ( 'NONE', ( #6672 ), #1620, .F. ) ;
#425=ORIENTED_EDGE ( 'NONE', *, *, #6234, .F. ) ;
#435=EDGE_CURVE ( 'NONE', #2310, #1809, #3699, .T. ) ;
#438=VERTEX_POINT ( 'NONE', #1523 ) ;
#440=ORIENTED_EDGE ( 'NONE', *, *, #6665, .T. ) ;
#441=EDGE_CURVE ( 'NONE', #2574, #8783, #903, .T. ) ;
#444=CARTESIAN_POINT ( 'NONE',  ( -27.00000000000000000, -43.00000000000000000, 11.99999999999999645 ) ) ;
#445=CARTESIAN_POINT ( 'NONE',  ( -27.00000000000000000, -43.00000000000000000, 11.99999999999999645 ) ) ;
#446=CARTESIAN_POINT ( 'NONE',  ( -38.00000000000000711, -43.00000000000000000, -7.366666666666667140 ) ) ;
#453=DIRECTION ( 'NONE',  ( 1.000000000000000000, 0.000000000000000000, 0.000000000000000000 ) ) ;
#455=DIRECTION ( 'NONE',  ( 0.000000000000000000, 0.7071067811865479058, -0.7071067811865472397 ) ) ;
#458=VERTEX_POINT ( 'NONE', #5126 ) ;
#465=ORIENTED_EDGE ( 'NONE', *, *, #9033, .T. ) ;
#467=DIRECTION ( 'NONE',  ( 0.000000000000000000, 0.000000000000000000, 1.000000000000000000 ) ) ;
#472=VERTEX_POINT ( 'NONE', #2965 ) ;
#473=CIRCLE ( 'NONE', #8880, 11.00000000000000000 ) ;
#476=CARTESIAN_POINT ( 'NONE',  ( -37.00000000000000711, -15.90990257669733943, -85.90990257669729147 ) ) ;
#477=LINE ( 'NONE', #4853, #2042 ) ;
#481=ORIENTED_EDGE ( 'NONE', *, *, #7216, .T. ) ;
#483=EDGE_CURVE ( 'NONE', #1534, #3407, #8098, .T. ) ;
#484=DIRECTION ( 'NONE',  ( -1.000000000000000000, 0.000000000000000000, 0.000000000000000000 ) ) ;
#486=DIRECTION ( 'NONE',  ( -1.000000000000000000, 0.000000000000000000, 0.000000000000000000 ) ) ;
#489=CARTESIAN_POINT ( 'NONE',  ( -19.74999999999999645, 43.00000000000000000, 25.00000000000000000 ) ) ;
#490=VERTEX_POINT ( 'NONE', #2874 ) ;
#495=VECTOR ( 'NONE', #924, 1000.000000000000000 ) ;
#497=CARTESIAN_POINT ( 'NONE',  ( -40.77961158827728383, -30.00000000000000000, -84.30964406271149869 ) ) ;
#507=CARTESIAN_POINT ( 'NONE',  ( 19.74999999999999645, 43.00000000000000000, 11.99999999999999645 ) ) ;
#512=CARTESIAN_POINT ( 'NONE',  ( 60.00000000000000000, 15.90990257669733943, -54.09009742330271564 ) ) ;
#520=AXIS2_PLACEMENT_3D ( 'NONE', #2674, #6231, #6948 ) ;
#521=CARTESIAN_POINT ( 'NONE',  ( 37.00000000000000000, 15.90990257669733943, -82.90990257669729147 ) ) ;
#522=CARTESIAN_POINT ( 'NONE',  ( -53.29490495164537833, 27.56180520566615044, -81.40266088840108694 ) ) ;
#523=VERTEX_POINT ( 'NONE', #5519 ) ;
#527=CARTESIAN_POINT ( 'NONE',  ( -34.25000000000000000, 43.00000000000000000, 25.00000000000000000 ) ) ;
#534=ADVANCED_FACE ( 'NONE', ( #8448, #1718, #6196, #5421, #992, #3880 ), #1862, .T. ) ;
#537=ORIENTED_EDGE ( 'NONE', *, *, #8121, .T. ) ;
#545=DIRECTION ( 'NONE',  ( -0.000000000000000000, -0.000000000000000000, -1.000000000000000000 ) ) ;
#550=VERTEX_POINT ( 'NONE', #234 ) ;
#551=DIRECTION ( 'NONE',  ( 1.000000000000000000, -0.000000000000000000, -0.000000000000000000 ) ) ;
#552=ORIENTED_EDGE ( 'NONE', *, *, #7615, .F. ) ;
#553=EDGE_CURVE ( 'NONE', #4380, #6251, #3112, .T. ) ;
#555=LINE ( 'NONE', #9438, #7175 ) ;
#559=CARTESIAN_POINT ( 'NONE',  ( 37.00000000000000000, 15.90990257669733943, -88.90990257669730568 ) ) ;
#568=AXIS2_PLACEMENT_3D ( 'NONE', #1834, #4046, #387 ) ;
#570=CONICAL_SURFACE ( 'NONE', #6720, 59.00000000000000000, 0.7853981633974415066 ) ;
#572=CIRCLE ( 'NONE', #5484, 7.250000000000002665 ) ;
#577=ORIENTED_EDGE ( 'NONE', *, *, #844, .F. ) ;
#580=VERTEX_POINT ( 'NONE', #8394 ) ;
#582=AXIS2_PLACEMENT_3D ( 'NONE', #2681, #3390, #5663 ) ;
#584=DIRECTION ( 'NONE',  ( -0.000000000000000000, -0.000000000000000000, 1.000000000000000000 ) ) ;
#587=VECTOR ( 'NONE', #7326, 1000.000000000000000 ) ;
#597=LINE ( 'NONE', #688, #3837 ) ;
#603=CARTESIAN_POINT ( 'NONE',  ( -38.00000000000000711, 43.00000000000000000, -7.366666666666667140 ) ) ;
#611=CARTESIAN_POINT ( 'NONE',  ( -15.99999999999999645, 43.00000000000000000, 11.99999999999999645 ) ) ;
#624=ORIENTED_EDGE ( 'NONE', *, *, #5824, .T. ) ;
#626=EDGE_LOOP ( 'NONE', ( #6551, #3598, #3305, #7283, #8776 ) ) ;
#629=CARTESIAN_POINT ( 'NONE',  ( 60.00000000000000000, -15.90990257669733943, -85.90990257669729147 ) ) ;
#633=EDGE_CURVE ( 'NONE', #6290, #6045, #8491, .T. ) ;
#636=CARTESIAN_POINT ( 'NONE',  ( -53.29490495164537833, -48.67545040036925741, -60.28901569369804747 ) ) ;
#645=VECTOR ( 'NONE', #5294, 1000.000000000000000 ) ;
#649=CARTESIAN_POINT ( 'NONE',  ( -51.96152422706632734, -30.00000000000000000, -134.0000000000000284 ) ) ;
#653=LINE ( 'NONE', #6518, #4120 ) ;
#657=EDGE_CURVE ( 'NONE', #4079, #8518, #4927, .T. ) ;
#663=LINE ( 'NONE', #1331, #1493 ) ;
#666=CARTESIAN_POINT ( 'NONE',  ( 60.00000000000000000, -30.00000000000000355, -82.50000000000001421 ) ) ;
#676=CARTESIAN_POINT ( 'NONE',  ( 53.29490495164537833, 15.90990257669733943, -54.09009742330271564 ) ) ;
#677=CARTESIAN_POINT ( 'NONE',  ( 0.000000000000000000, 30.00000000000000000, 0.000000000000000000 ) ) ;
#681=EDGE_LOOP ( 'NONE', ( #2078, #3194, #2258, #7181 ) ) ;
#685=CARTESIAN_POINT ( 'NONE',  ( 38.00000000000000711, 21.00000000000000000, -16.89999999999999858 ) ) ;
#688=CARTESIAN_POINT ( 'NONE',  ( -52.83333333333332860, 1.666666666666670515, -110.8333333333333570 ) ) ;
#691=VECTOR ( 'NONE', #2336, 1000.000000000000000 ) ;
#699=ORIENTED_EDGE ( 'NONE', *, *, #1430, .T. ) ;
#704=ORIENTED_EDGE ( 'NONE', *, *, #4777, .T. ) ;
#706=CARTESIAN_POINT ( 'NONE',  ( -53.29490495164537833, -48.67545040036925741, -60.28901569369804747 ) ) ;
#710=VECTOR ( 'NONE', #3242, 1000.000000000000000 ) ;
#712=PLANE ( 'NONE',  #4815 ) ;
#718=ORIENTED_EDGE ( 'NONE', *, *, #258, .T. ) ;
#721=CIRCLE ( 'NONE', #4560, 15.00000000000000000 ) ;
#727=CARTESIAN_POINT ( 'NONE',  ( 27.00000000000000000, 43.00000000000000000, 11.99999999999999645 ) ) ;
#728=EDGE_CURVE ( 'NONE', #4995, #5609, #7000, .T. ) ;
#730=DIRECTION ( 'NONE',  ( -1.000000000000000000, 0.000000000000000000, 0.000000000000000000 ) ) ;
#731=EDGE_CURVE ( 'NONE', #4380, #8166, #801, .T. ) ;
#738=DIRECTION ( 'NONE',  ( 0.000000000000000000, 0.000000000000000000, 1.000000000000000000 ) ) ;
#741=EDGE_LOOP ( 'NONE', ( #8352, #2791, #1869, #1604 ) ) ;
#746=CIRCLE ( 'NONE', #4747, 3.000000000000002665 ) ;
#748=AXIS2_PLACEMENT_3D ( 'NONE', #2990, #3859, #8037 ) ;
#749=LINE ( 'NONE', #6766, #8751 ) ;
#753=EDGE_CURVE ( 'NONE', #2323, #490, #5614, .T. ) ;
#755=ORIENTED_EDGE ( 'NONE', *, *, #7404, .T. ) ;
#757=CYLINDRICAL_SURFACE ( 'NONE', #4580, 3.000000000000002665 ) ;
#766=ORIENTED_EDGE ( 'NONE', *, *, #4400, .F. ) ;
#770=PLANE ( 'NONE',  #2650 ) ;
#772=DIRECTION ( 'NONE',  ( -0.000000000000000000, -0.000000000000000000, -1.000000000000000000 ) ) ;
#788=DIRECTION ( 'NONE',  ( -1.000000000000000000, 0.000000000000000000, -0.000000000000000000 ) ) ;
#789=LINE ( 'NONE', #8960, #1229 ) ;
#790=PLANE ( 'NONE',  #984 ) ;
#795=CARTESIAN_POINT ( 'NONE',  ( -27.00000000000000000, -43.00000000000000000, -25.00000000000000000 ) ) ;
#800=EDGE_CURVE ( 'NONE', #6840, #1397, #8148, .T. ) ;
#801=( BOUNDED_CURVE ( )  B_SPLINE_CURVE ( 3, ( #4118, #3434, #4883, #1224 ),
 .UNSPECIFIED., .F., .T. ) 
 B_SPLINE_CURVE_WITH_KNOTS ( ( 4, 4 ),
 ( 3.213317012039606180, 4.712388980384689674 ),
 .UNSPECIFIED. ) 
 CURVE ( )  GEOMETRIC_REPRESENTATION_ITEM ( )  RATIONAL_B_SPLINE_CURVE ( ( 1.000000000000000000, 0.8213367208436765932, 0.8213367208436765932, 1.000000000000000000 ) ) 
 REPRESENTATION_ITEM ( '' )  );
#802=DIRECTION ( 'NONE',  ( 0.5773502691896252870, -0.5773502691896258421, -0.5773502691896261751 ) ) ;
#804=VERTEX_POINT ( 'NONE', #2228 ) ;
#805=EDGE_CURVE ( 'NONE', #6613, #5515, #7492, .T. ) ;
#815=FACE_OUTER_BOUND ( 'NONE', #6771, .T. ) ;
#818=LINE ( 'NONE', #922, #8704 ) ;
#821=CARTESIAN_POINT ( 'NONE',  ( 37.00000000000000000, -15.90990257669733943, -57.09009742330271564 ) ) ;
#824=ADVANCED_FACE ( 'NONE', ( #76 ), #3055, .F. ) ;
#830=EDGE_CURVE ( 'NONE', #75, #6840, #1791, .T. ) ;
#835=LINE ( 'NONE', #3769, #2450 ) ;
#836=DIRECTION ( 'NONE',  ( -1.000000000000000000, -0.000000000000000000, -0.000000000000000000 ) ) ;
#837=CARTESIAN_POINT ( 'NONE',  ( 37.00000000000000000, -15.90990257669733943, -54.09009742330271564 ) ) ;
#844=EDGE_CURVE ( 'NONE', #2915, #287, #5888, .T. ) ;
#845=ORIENTED_EDGE ( 'NONE', *, *, #6602, .T. ) ;
#846=ORIENTED_EDGE ( 'NONE', *, *, #9070, .T. ) ;
#850=ORIENTED_EDGE ( 'NONE', *, *, #8658, .F. ) ;
#854=CARTESIAN_POINT ( 'NONE',  ( 60.00000000000000000, -12.50000000000000000, -100.0000000000000000 ) ) ;
#856=ORIENTED_EDGE ( 'NONE', *, *, #2427, .F. ) ;
#857=ORIENTED_EDGE ( 'NONE', *, *, #4299, .T. ) ;
#859=CYLINDRICAL_SURFACE ( 'NONE', #2232, 11.00000000000000000 ) ;
#865=CARTESIAN_POINT ( 'NONE',  ( 60.00000000000000000, -15.90990257669733943, -54.09009742330271564 ) ) ;
#867=DIRECTION ( 'NONE',  ( 0.000000000000000000, 1.000000000000000000, 0.000000000000000000 ) ) ;
#870=ORIENTED_EDGE ( 'NONE', *, *, #6924, .F. ) ;
#876=AXIS2_PLACEMENT_3D ( 'NONE', #3595, #3018, #2251 ) ;
#881=VECTOR ( 'NONE', #2152, 1000.000000000000000 ) ;
#892=EDGE_CURVE ( 'NONE', #6251, #3861, #7658, .T. ) ;
#893=CIRCLE ( 'NONE', #9021, 7.250000000000002665 ) ;
#894=EDGE_CURVE ( 'NONE', #1738, #8284, #835, .T. ) ;
#896=LINE ( 'NONE', #3824, #3532 ) ;
#899=CARTESIAN_POINT ( 'NONE',  ( 27.00000000000000000, -43.00000000000000000, 11.99999999999999645 ) ) ;
#900=VERTEX_POINT ( 'NONE', #127 ) ;
#903=LINE ( 'NONE', #4459, #5794 ) ;
#910=ORIENTED_EDGE ( 'NONE', *, *, #3003, .F. ) ;
#913=EDGE_CURVE ( 'NONE', #1970, #4478, #7805, .T. ) ;
#915=DIRECTION ( 'NONE',  ( -0.000000000000000000, 1.000000000000000000, 0.000000000000000000 ) ) ;
#917=FACE_OUTER_BOUND ( 'NONE', #7223, .T. ) ;
#922=CARTESIAN_POINT ( 'NONE',  ( 60.00000000000000000, -15.90990257669733943, -88.90990257669730568 ) ) ;
#923=ORIENTED_EDGE ( 'NONE', *, *, #5717, .F. ) ;
#924=DIRECTION ( 'NONE',  ( 0.000000000000000000, 0.000000000000000000, -1.000000000000000000 ) ) ;
#927=ADVANCED_FACE ( 'NONE', ( #6803 ), #8330, .F. ) ;
#932=EDGE_CURVE ( 'NONE', #3514, #2323, #9167, .T. ) ;
#935=DIRECTION ( 'NONE',  ( -1.000000000000000000, 0.000000000000000000, 0.000000000000000000 ) ) ;
#936=CARTESIAN_POINT ( 'NONE',  ( 53.29490495164537833, -3.673940397442057600E-15, -70.00000000000000000 ) ) ;
#937=VECTOR ( 'NONE', #455, 999.9999999999998863 ) ;
#938=FACE_OUTER_BOUND ( 'NONE', #5383, .T. ) ;
#941=DIRECTION ( 'NONE',  ( 0.7071067811865450192, -0.5000000000000019984, 0.5000000000000016653 ) ) ;
#944=ORIENTED_EDGE ( 'NONE', *, *, #2603, .T. ) ;
#945=FACE_OUTER_BOUND ( 'NONE', #6900, .T. ) ;
#946=EDGE_LOOP ( 'NONE', ( #4686, #3454, #2994, #6192 ) ) ;
#949=DIRECTION ( 'NONE',  ( -1.000000000000000000, -0.000000000000000000, -0.000000000000000000 ) ) ;
#951=( BOUNDED_CURVE ( )  B_SPLINE_CURVE ( 3, ( #8151, #3772, #8047, #1564 ),
 .UNSPECIFIED., .F., .F. ) 
 B_SPLINE_CURVE_WITH_KNOTS ( ( 4, 4 ),
 ( 5.805906910357376383, 6.283185307179586232 ),
 .UNSPECIFIED. ) 
 CURVE ( )  GEOMETRIC_REPRESENTATION_ITEM ( )  RATIONAL_B_SPLINE_CURVE ( ( 1.000000000000000000, 0.9811070276743185659, 0.9811070276743185659, 1.000000000000000000 ) ) 
 REPRESENTATION_ITEM ( '' )  );
#952=EDGE_CURVE ( 'NONE', #3120, #5090, #746, .T. ) ;
#953=DIRECTION ( 'NONE',  ( 1.000000000000000000, -0.000000000000000000, -0.000000000000000000 ) ) ;
#955=VERTEX_POINT ( 'NONE', #175 ) ;
#959=VECTOR ( 'NONE', #9416, 1000.000000000000000 ) ;
#960=DIRECTION ( 'NONE',  ( -0.000000000000000000, -0.000000000000000000, -1.000000000000000000 ) ) ;
#961=DIRECTION ( 'NONE',  ( -1.000000000000000000, 0.000000000000000000, -0.000000000000000000 ) ) ;
#962=CARTESIAN_POINT ( 'NONE',  ( -60.00000000000000000, 30.00000000000000000, -13.00000000000000000 ) ) ;
#963=DIRECTION ( 'NONE',  ( -1.000000000000000000, 0.000000000000000000, 0.000000000000000000 ) ) ;
#964=VECTOR ( 'NONE', #2804, 1000.000000000000000 ) ;
#971=DIRECTION ( 'NONE',  ( 0.000000000000000000, 0.000000000000000000, -1.000000000000000000 ) ) ;
#973=LINE ( 'NONE', #3323, #1059 ) ;
#974=CARTESIAN_POINT ( 'NONE',  ( -38.00000000000000711, -44.39318849903268926, -6.762951650419163130 ) ) ;
#975=VERTEX_POINT ( 'NONE', #1029 ) ;
#979=CARTESIAN_POINT ( 'NONE',  ( 60.00000000000001421, -9.637301612213114765, -29.99999999999998934 ) ) ;
#984=AXIS2_PLACEMENT_3D ( 'NONE', #2233, #6767, #6857 ) ;
#986=FACE_OUTER_BOUND ( 'NONE', #5203, .T. ) ;
#992=FACE_OUTER_BOUND ( 'NONE', #9110, .T. ) ;
#997=CYLINDRICAL_SURFACE ( 'NONE', #9161, 3.000000000000002665 ) ;
#998=FACE_BOUND ( 'NONE', #1821, .T. ) ;
#999=CYLINDRICAL_SURFACE ( 'NONE', #5801, 3.000000000000002665 ) ;
#1004=EDGE_CURVE ( 'NONE', #4533, #1970, #8239, .T. ) ;
#1006=DIRECTION ( 'NONE',  ( 1.000000000000000000, 0.000000000000000000, 0.000000000000000000 ) ) ;
#1009=EDGE_CURVE ( 'NONE', #301, #8237, #3646, .T. ) ;
#1011=( LENGTH_UNIT ( ) NAMED_UNIT ( * ) SI_UNIT ( .MILLI., .METRE. ) );
#1015=DIRECTION ( 'NONE',  ( -1.000000000000000000, 0.000000000000000000, 0.000000000000000000 ) ) ;
#1016=ORIENTED_EDGE ( 'NONE', *, *, #435, .T. ) ;
#1017=VECTOR ( 'NONE', #6765, 1000.000000000000000 ) ;
#1018=PLANE ( 'NONE',  #1104 ) ;
#1021=CARTESIAN_POINT ( 'NONE',  ( -37.73845885098650399, -45.76160744848117190, -6.169970105658154402 ) ) ;
#1025=ORIENTED_EDGE ( 'NONE', *, *, #5159, .F. ) ;
#1026=ORIENTED_EDGE ( 'NONE', *, *, #4417, .T. ) ;
#1027=ORIENTED_EDGE ( 'NONE', *, *, #7993, .T. ) ;
#1029=CARTESIAN_POINT ( 'NONE',  ( 60.00000000000000000, 7.347880794884118356E-15, 23.99999999999998579 ) ) ;
#1031=EDGE_CURVE ( 'NONE', #4623, #5090, #6140, .T. ) ;
#1033=LINE ( 'NONE', #5507, #1636 ) ;
#1036=AXIS2_PLACEMENT_3D ( 'NONE', #5375, #941, #7472 ) ;
#1046=( GEOMETRIC_REPRESENTATION_CONTEXT ( 3 ) GLOBAL_UNCERTAINTY_ASSIGNED_CONTEXT ( ( #2403 ) ) GLOBAL_UNIT_ASSIGNED_CONTEXT ( ( #1011, #6067, #4619 ) ) REPRESENTATION_CONTEXT ( 'NONE', 'WORKASPACE' ) );
#1049=EDGE_CURVE ( 'NONE', #3283, #8519, #7962, .T. ) ;
#1050=PLANE ( 'NONE',  #5443 ) ;
#1056=PRODUCT_CONTEXT ( 'NONE', #6585, 'mechanical' ) ;
#1057=VECTOR ( 'NONE', #5268, 1000.000000000000000 ) ;
#1059=VECTOR ( 'NONE', #7701, 1000.000000000000000 ) ;
#1061=DIRECTION ( 'NONE',  ( -1.000000000000000000, 0.000000000000000000, 0.000000000000000000 ) ) ;
#1066=ORIENTED_EDGE ( 'NONE', *, *, #7565, .F. ) ;
#1067=DIRECTION ( 'NONE',  ( 0.000000000000000000, 0.000000000000000000, -1.000000000000000000 ) ) ;
#1070=CIRCLE ( 'NONE', #162, 7.250000000000002665 ) ;
#1071=CARTESIAN_POINT ( 'NONE',  ( 43.18827341296427846, -42.33902489539482161, -7.653089211995572683 ) ) ;
#1073=EDGE_LOOP ( 'NONE', ( #3291, #1027, #5277, #3734 ) ) ;
#1074=ORIENTED_EDGE ( 'NONE', *, *, #2810, .F. ) ;
#1075=ORIENTED_EDGE ( 'NONE', *, *, #1004, .F. ) ;
#1076=VERTEX_POINT ( 'NONE', #4519 ) ;
#1080=CARTESIAN_POINT ( 'NONE',  ( 40.05867498135629745, -15.23141075423630575, -98.05867498135631877 ) ) ;
#1089=CARTESIAN_POINT ( 'NONE',  ( 52.42476942962458963, -29.19763577280656008, -80.99738777760515518 ) ) ;
#1092=EDGE_LOOP ( 'NONE', ( #2816, #8479 ) ) ;
#1098=CIRCLE ( 'NONE', #196, 59.00000000000000000 ) ;
#1099=CARTESIAN_POINT ( 'NONE',  ( -51.96152422706632734, 30.00000000000000000, -80.85015119857381194 ) ) ;
#1101=CARTESIAN_POINT ( 'NONE',  ( -39.50000000000000711, -14.99999999999999289, -97.50000000000001421 ) ) ;
#1104=AXIS2_PLACEMENT_3D ( 'NONE', #303, #8278, #3956 ) ;
#1106=LINE ( 'NONE', #2561, #7473 ) ;
#1110=AXIS2_PLACEMENT_3D ( 'NONE', #400, #4914, #453 ) ;
#1111=EDGE_CURVE ( 'NONE', #3876, #7733, #7502, .T. ) ;
#1131=DIRECTION ( 'NONE',  ( -0.7071067811865445751, 0.5000000000000019984, 0.5000000000000024425 ) ) ;
#1132=VERTEX_POINT ( 'NONE', #14 ) ;
#1136=EDGE_LOOP ( 'NONE', ( #4865, #8916, #3783, #8298 ) ) ;
#1139=ADVANCED_FACE ( 'NONE', ( #2318 ), #8173, .F. ) ;
#1143=ADVANCED_FACE ( 'NONE', ( #815 ), #2367, .F. ) ;
#1147=CARTESIAN_POINT ( 'NONE',  ( 38.00000000000000000, -43.00000000000000000, 11.99999999999999645 ) ) ;
#1151=AXIS2_PLACEMENT_3D ( 'NONE', #1715, #6193, #5467 ) ;
#1153=EDGE_LOOP ( 'NONE', ( #3979, #2206 ) ) ;
#1156=DIRECTION ( 'NONE',  ( -0.000000000000000000, -0.000000000000000000, -1.000000000000000000 ) ) ;
#1160=FACE_BOUND ( 'NONE', #7575, .T. ) ;
#1162=VECTOR ( 'NONE', #8268, 1000.000000000000000 ) ;
#1175=DIRECTION ( 'NONE',  ( 1.000000000000000000, 0.000000000000000000, 0.000000000000000000 ) ) ;
#1176=ORIENTED_EDGE ( 'NONE', *, *, #3653, .T. ) ;
#1179=DIRECTION ( 'NONE',  ( -1.000000000000000000, 0.000000000000000000, 0.000000000000000000 ) ) ;
#1181=ADVANCED_FACE ( 'NONE', ( #8793 ), #2213, .F. ) ;
#1191=VECTOR ( 'NONE', #191, 1000.000000000000000 ) ;
#1197=LINE ( 'NONE', #4988, #6656 ) ;
#1198=CARTESIAN_POINT ( 'NONE',  ( -52.86930915046633572, 28.38475884032111196, -81.18159060786257442 ) ) ;
#1210=ORIENTED_EDGE ( 'NONE', *, *, #2888, .F. ) ;
#1211=VERTEX_POINT ( 'NONE', #4574 ) ;
#1219=CARTESIAN_POINT ( 'NONE',  ( -15.99999999999999645, -43.00000000000000000, 11.99999999999999645 ) ) ;
#1224=CARTESIAN_POINT ( 'NONE',  ( 16.00000000000000000, -43.00000000000000000, -7.366666666666667140 ) ) ;
#1229=VECTOR ( 'NONE', #7520, 1000.000000000000000 ) ;
#1231=ORIENTED_EDGE ( 'NONE', *, *, #2888, .T. ) ;
#1232=ORIENTED_EDGE ( 'NONE', *, *, #1031, .F. ) ;
#1235=ADVANCED_FACE ( 'NONE', ( #299 ), #3268, .F. ) ;
#1239=FACE_OUTER_BOUND ( 'NONE', #6000, .T. ) ;
#1245=ORIENTED_EDGE ( 'NONE', *, *, #4252, .T. ) ;
#1247=VECTOR ( 'NONE', #4632, 1000.000000000000000 ) ;
#1255=ORIENTED_EDGE ( 'NONE', *, *, #306, .T. ) ;
#1264=ORIENTED_EDGE ( 'NONE', *, *, #349, .T. ) ;
#1269=CYLINDRICAL_SURFACE ( 'NONE', #1321, 7.250000000000002665 ) ;
#1275=ORIENTED_EDGE ( 'NONE', *, *, #6263, .T. ) ;
#1277=CARTESIAN_POINT ( 'NONE',  ( 19.74999999999999645, -43.00000000000000000, -25.00000000000000000 ) ) ;
#1282=CIRCLE ( 'NONE', #3145, 3.000000000000002665 ) ;
#1283=CARTESIAN_POINT ( 'NONE',  ( 53.29490495164537833, 15.90990257669733943, -88.90990257669730568 ) ) ;
#1292=AXIS2_PLACEMENT_3D ( 'NONE', #476, #7099, #7062 ) ;
#1298=DIRECTION ( 'NONE',  ( 0.000000000000000000, 0.000000000000000000, -1.000000000000000000 ) ) ;
#1300=DIRECTION ( 'NONE',  ( 1.000000000000000000, 0.000000000000000000, 0.000000000000000000 ) ) ;
#1301=ORIENTED_EDGE ( 'NONE', *, *, #7281, .T. ) ;
#1302=CARTESIAN_POINT ( 'NONE',  ( -60.00000000000000000, 0.000000000000000000, -30.00000000000000000 ) ) ;
#1303=ORIENTED_EDGE ( 'NONE', *, *, #830, .F. ) ;
#1311=VECTOR ( 'NONE', #5911, 1000.000000000000000 ) ;
#1312=DIRECTION ( 'NONE',  ( -0.7071067811865435759, 0.000000000000000000, 0.7071067811865514585 ) ) ;
#1313=ORIENTED_EDGE ( 'NONE', *, *, #4357, .F. ) ;
#1315=ORIENTED_EDGE ( 'NONE', *, *, #728, .F. ) ;
#1316=CARTESIAN_POINT ( 'NONE',  ( 37.00000000000000000, -15.90990257669733943, -54.09009742330271564 ) ) ;
#1321=AXIS2_PLACEMENT_3D ( 'NONE', #8626, #5799, #9393 ) ;
#1323=CARTESIAN_POINT ( 'NONE',  ( -38.00000000000000711, 43.00000000000000000, -7.366666666666667140 ) ) ;
#1324=CARTESIAN_POINT ( 'NONE',  ( -27.00000000000000000, 43.00000000000000000, 11.99999999999999645 ) ) ;
#1326=CARTESIAN_POINT ( 'NONE',  ( -38.00000000000000711, 43.00000000000000000, -7.366666666666667140 ) ) ;
#1327=CIRCLE ( 'NONE', #6708, 3.000000000000002665 ) ;
#1331=CARTESIAN_POINT ( 'NONE',  ( -51.96152422706632734, 30.00000000000000000, -134.0000000000000284 ) ) ;
#1334=DIRECTION ( 'NONE',  ( -1.000000000000000000, 0.000000000000000000, 0.000000000000000000 ) ) ;
#1340=ORIENTED_EDGE ( 'NONE', *, *, #9033, .F. ) ;
#1341=EDGE_CURVE ( 'NONE', #5088, #1397, #4987, .T. ) ;
#1343=ORIENTED_EDGE ( 'NONE', *, *, #6945, .F. ) ;
#1345=ORIENTED_EDGE ( 'NONE', *, *, #153, .F. ) ;
#1361=CARTESIAN_POINT ( 'NONE',  ( 37.22467645238199196, 47.05659850664387278, -5.608807313787652404 ) ) ;
#1363=LINE ( 'NONE', #1455, #9425 ) ;
#1366=ORIENTED_EDGE ( 'NONE', *, *, #2068, .T. ) ;
#1369=CARTESIAN_POINT ( 'NONE',  ( 27.00000000000000000, -43.00000000000000000, 11.99999999999999645 ) ) ;
#1372=CARTESIAN_POINT ( 'NONE',  ( 60.00000000000000000, -15.90990257669733943, -85.90990257669729147 ) ) ;
#1375=CIRCLE ( 'NONE', #5968, 60.00000000000000000 ) ;
#1376=DIRECTION ( 'NONE',  ( 1.000000000000000000, -0.000000000000000000, -0.000000000000000000 ) ) ;
#1379=ORIENTED_EDGE ( 'NONE', *, *, #4011, .T. ) ;
#1389=CIRCLE ( 'NONE', #3853, 15.00000000000000000 ) ;
#1391=DIRECTION ( 'NONE',  ( 1.000000000000000000, -0.000000000000000000, -0.000000000000000000 ) ) ;
#1397=VERTEX_POINT ( 'NONE', #522 ) ;
#1398=CARTESIAN_POINT ( 'NONE',  ( 37.00000000000000000, 30.00000000000000000, -13.00000000000001066 ) ) ;
#1399=ORIENTED_EDGE ( 'NONE', *, *, #5814, .T. ) ;
#1400=AXIS2_PLACEMENT_3D ( 'NONE', #5402, #4096, #9184 ) ;
#1404=DIRECTION ( 'NONE',  ( 0.000000000000000000, 0.7071067811865479058, -0.7071067811865472397 ) ) ;
#1405=CARTESIAN_POINT ( 'NONE',  ( 48.15955140082796504, 36.58521010404106732, -10.14640895491553252 ) ) ;
#1411=ORIENTED_EDGE ( 'NONE', *, *, #3657, .F. ) ;
#1412=DIRECTION ( 'NONE',  ( 0.6785983445458485530, -0.2810846377148105701, 0.6785983445458495522 ) ) ;
#1416=ADVANCED_FACE ( 'NONE', ( #7064 ), #3449, .F. ) ;
#1420=VECTOR ( 'NONE', #5369, 1000.000000000000114 ) ;
#1425=CARTESIAN_POINT ( 'NONE',  ( -15.99999999999999645, -43.00000000000000000, -7.366666666666667140 ) ) ;
#1426=EDGE_CURVE ( 'NONE', #4458, #95, #2789, .T. ) ;
#1427=VECTOR ( 'NONE', #1736, 1000.000000000000000 ) ;
#1430=EDGE_CURVE ( 'NONE', #6915, #2915, #1491, .T. ) ;
#1431=LINE ( 'NONE', #5084, #4054 ) ;
#1435=VERTEX_POINT ( 'NONE', #3365 ) ;
#1438=VECTOR ( 'NONE', #8497, 1000.000000000000000 ) ;
#1440=FACE_OUTER_BOUND ( 'NONE', #5060, .T. ) ;
#1441=AXIS2_PLACEMENT_3D ( 'NONE', #7017, #9256, #2015 ) ;
#1443=DIRECTION ( 'NONE',  ( -1.000000000000000000, 0.000000000000000000, 0.000000000000000000 ) ) ;
#1449=VECTOR ( 'NONE', #5531, 999.9999999999998863 ) ;
#1450=ORIENTED_EDGE ( 'NONE', *, *, #6945, .T. ) ;
#1455=CARTESIAN_POINT ( 'NONE',  ( 60.00000000000000000, 12.50000000000000000, -100.0000000000000000 ) ) ;
#1461=DIRECTION ( 'NONE',  ( -1.000000000000000000, 0.000000000000000000, 0.000000000000000000 ) ) ;
#1463=DIRECTION ( 'NONE',  ( 0.000000000000000000, 0.000000000000000000, -1.000000000000000000 ) ) ;
#1468=CARTESIAN_POINT ( 'NONE',  ( -53.29490495164537833, 15.90990257669733943, -85.90990257669729147 ) ) ;
#1472=AXIS2_PLACEMENT_3D ( 'NONE', #1372, #2820, #4887 ) ;
#1477=DIRECTION ( 'NONE',  ( 1.000000000000000000, 0.000000000000000000, 0.000000000000000000 ) ) ;
#1479=CARTESIAN_POINT ( 'NONE',  ( -53.29490495164537833, -27.56180520566615044, -41.61356529332876875 ) ) ;
#1481=EDGE_LOOP ( 'NONE', ( #3444, #9188, #552, #1232 ) ) ;
#1483=AXIS2_PLACEMENT_3D ( 'NONE', #7199, #7831, #8644 ) ;
#1487=DIRECTION ( 'NONE',  ( 0.000000000000000000, 0.000000000000000000, -1.000000000000000000 ) ) ;
#1488=DIRECTION ( 'NONE',  ( -0.000000000000000000, -0.000000000000000000, 1.000000000000000000 ) ) ;
#1490=CARTESIAN_POINT ( 'NONE',  ( 53.29490495164537833, -3.673940397442057600E-15, -55.00000000000000711 ) ) ;
#1491=CIRCLE ( 'NONE', #1483, 3.000000000000002665 ) ;
#1493=VECTOR ( 'NONE', #6527, 1000.000000000000000 ) ;
#1501=CARTESIAN_POINT ( 'NONE',  ( -27.00000000000000000, 43.00000000000000000, 11.99999999999999645 ) ) ;
#1508=LINE ( 'NONE', #649, #691 ) ;
#1510=ADVANCED_FACE ( 'NONE', ( #5185 ), #2308, .T. ) ;
#1514=DIRECTION ( 'NONE',  ( 0.000000000000000000, 0.000000000000000000, 1.000000000000000000 ) ) ;
#1517=EDGE_CURVE ( 'NONE', #5309, #75, #5918, .T. ) ;
#1523=CARTESIAN_POINT ( 'NONE',  ( -53.29490495164537833, -15.90990257669733943, -82.90990257669729147 ) ) ;
#1524=ORIENTED_EDGE ( 'NONE', *, *, #2533, .F. ) ;
#1527=FACE_BOUND ( 'NONE', #8238, .T. ) ;
#1534=VERTEX_POINT ( 'NONE', #5135 ) ;
#1536=EDGE_CURVE ( 'NONE', #313, #1132, #7937, .T. ) ;
#1545=EDGE_LOOP ( 'NONE', ( #4724, #465, #3693, #6289 ) ) ;
#1548=CARTESIAN_POINT ( 'NONE',  ( 16.00000000000000000, -43.00000000000000000, -7.366666666666667140 ) ) ;
#1552=CARTESIAN_POINT ( 'NONE',  ( -59.00000000000000000, 0.000000000000000000, 25.00000000000000000 ) ) ;
#1554=EDGE_CURVE ( 'NONE', #2195, #4316, #3741, .T. ) ;
#1561=VERTEX_POINT ( 'NONE', #2156 ) ;
#1564=CARTESIAN_POINT ( 'NONE',  ( 60.00000000000000000, 7.347880794884118356E-15, -30.00000000000000000 ) ) ;
#1572=CARTESIAN_POINT ( 'NONE',  ( 26.21170834203229916, 53.97171801779367684, 11.99999999999999645 ) ) ;
#1577=DIRECTION ( 'NONE',  ( 0.000000000000000000, 0.7071067811865479058, -0.7071067811865472397 ) ) ;
#1587=FACE_OUTER_BOUND ( 'NONE', #2085, .T. ) ;
#1588=DIRECTION ( 'NONE',  ( -0.7071067811865481278, 0.4999999999999994449, 0.4999999999999998890 ) ) ;
#1591=CARTESIAN_POINT ( 'NONE',  ( 53.29490495164537833, -30.00000000000000000, -97.50000000000002842 ) ) ;
#1592=EDGE_LOOP ( 'NONE', ( #4138, #3431, #5308, #1026 ) ) ;
#1604=ORIENTED_EDGE ( 'NONE', *, *, #9381, .F. ) ;
#1607=EDGE_LOOP ( 'NONE', ( #6203, #4707 ) ) ;
#1609=CARTESIAN_POINT ( 'NONE',  ( -53.29490495164537833, 27.56180520566615044, -41.61356529332876875 ) ) ;
#1610=ADVANCED_FACE ( 'NONE', ( #5285 ), #7583, .F. ) ;
#1611=CARTESIAN_POINT ( 'NONE',  ( 60.00000000000000000, 29.99999999999999645, -82.50000000000000000 ) ) ;
#1614=AXIS2_PLACEMENT_3D ( 'NONE', #6760, #5504, #4539 ) ;
#1615=EDGE_CURVE ( 'NONE', #2574, #1684, #9069, .T. ) ;
#1620=PLANE ( 'NONE',  #7629 ) ;
#1629=CIRCLE ( 'NONE', #3005, 3.000000000000002665 ) ;
#1630=ORIENTED_EDGE ( 'NONE', *, *, #4418, .F. ) ;
#1634=DIRECTION ( 'NONE',  ( -1.000000000000000000, 0.000000000000000000, 0.000000000000000000 ) ) ;
#1635=CARTESIAN_POINT ( 'NONE',  ( -48.15955140082797925, -36.58521010404104601, -10.14640895491554140 ) ) ;
#1636=VECTOR ( 'NONE', #8439, 1000.000000000000000 ) ;
#1639=ADVANCED_FACE ( 'NONE', ( #1820 ), #999, .F. ) ;
#1644=CLOSED_SHELL ( 'NONE', ( #8760, #7621, #5555, #5827, #927, #4656, #7916, #824, #6704, #6175, #2946, #7723, #2782, #8654, #7705, #1610, #2011, #3314, #8933, #6967, #3771, #407, #1416, #8175, #7328, #7348, #2665, #2714, #3972, #3510, #1510, #534, #9108, #6120, #3001, #6533, #1757, #7842, #7935, #9358, #2352, #3179, #4532, #9330, #5320, #2830, #6255, #8721, #7227, #5933, #8029, #4759, #2549, #125, #3190, #8065, #2618, #253, #4658, #4012, #4843, #1235, #9235, #6342, #6419, #5736, #2239, #1639, #3706, #7040, #2244, #423, #9312, #1139, #2446, #3219, #1181, #9054, #1143, #4999 ) ) ;
#1645=ORIENTED_EDGE ( 'NONE', *, *, #9118, .F. ) ;
#1646=DIRECTION ( 'NONE',  ( -1.000000000000000000, 0.000000000000000000, 0.000000000000000000 ) ) ;
#1649=DIRECTION ( 'NONE',  ( -0.000000000000000000, 1.000000000000000000, 0.000000000000000000 ) ) ;
#1655=AXIS2_PLACEMENT_3D ( 'NONE', #7536, #949, #3883 ) ;
#1664=DIRECTION ( 'NONE',  ( 0.000000000000000000, 0.000000000000000000, 1.000000000000000000 ) ) ;
#1665=VECTOR ( 'NONE', #2243, 1000.000000000000000 ) ;
#1668=CARTESIAN_POINT ( 'NONE',  ( -37.00000000000000711, 15.90990257669733943, -51.09009742330271564 ) ) ;
#1671=DIRECTION ( 'NONE',  ( 0.000000000000000000, 0.000000000000000000, 1.000000000000000000 ) ) ;
#1675=AXIS2_PLACEMENT_3D ( 'NONE', #3606, #158, #58 ) ;
#1678=APPLICATION_CONTEXT ( 'automotive_design' ) ;
#1682=CARTESIAN_POINT ( 'NONE',  ( 61.20398523554579384, 8.188417774577869679, -89.59091971609970528 ) ) ;
#1684=VERTEX_POINT ( 'NONE', #4034 ) ;
#1689=CARTESIAN_POINT ( 'NONE',  ( -53.29490495164537833, -15.90990257669733943, -51.09009742330271564 ) ) ;
#1691=DIRECTION ( 'NONE',  ( 0.000000000000000000, -0.7071067811865479058, 0.7071067811865472397 ) ) ;
#1698=CARTESIAN_POINT ( 'NONE',  ( 53.29490495164537833, 15.90990257669733943, -51.09009742330271564 ) ) ;
#1700=EDGE_LOOP ( 'NONE', ( #5140, #6310, #1016, #5227 ) ) ;
#1704=DIRECTION ( 'NONE',  ( 0.000000000000000000, 0.000000000000000000, 1.000000000000000000 ) ) ;
#1706=CIRCLE ( 'NONE', #5396, 3.000000000000002665 ) ;
#1714=ORIENTED_EDGE ( 'NONE', *, *, #1049, .T. ) ;
#1715=CARTESIAN_POINT ( 'NONE',  ( 0.000000000000000000, 0.000000000000000000, 11.99999999999999645 ) ) ;
#1716=ORIENTED_EDGE ( 'NONE', *, *, #2452, .T. ) ;
#1718=FACE_BOUND ( 'NONE', #7249, .T. ) ;
#1736=DIRECTION ( 'NONE',  ( -0.000000000000000000, -0.000000000000000000, 1.000000000000000000 ) ) ;
#1738=VERTEX_POINT ( 'NONE', #8543 ) ;
#1739=FACE_OUTER_BOUND ( 'NONE', #3588, .T. ) ;
#1743=CARTESIAN_POINT ( 'NONE',  ( 60.00000000000000000, 29.99999999999999645, -82.50000000000000000 ) ) ;
#1744=ORIENTED_EDGE ( 'NONE', *, *, #325, .T. ) ;
#1752=EDGE_CURVE ( 'NONE', #3888, #2481, #7518, .T. ) ;
#1757=ADVANCED_FACE ( 'NONE', ( #7008 ), #2738, .T. ) ;
#1759=EDGE_LOOP ( 'NONE', ( #243, #1379, #8307, #3835 ) ) ;
#1760=CIRCLE ( 'NONE', #1913, 3.000000000000002665 ) ;
#1761=ORIENTED_EDGE ( 'NONE', *, *, #4826, .F. ) ;
#1768=CYLINDRICAL_SURFACE ( 'NONE', #8201, 11.00000000000000000 ) ;
#1770=ORIENTED_EDGE ( 'NONE', *, *, #3518, .F. ) ;
#1771=EDGE_LOOP ( 'NONE', ( #4684, #5251, #5302, #6564 ) ) ;
#1778=CARTESIAN_POINT ( 'NONE',  ( 0.000000000000000000, 0.000000000000000000, 25.00000000000000000 ) ) ;
#1782=LINE ( 'NONE', #4723, #3333 ) ;
#1783=ORIENTED_EDGE ( 'NONE', *, *, #3897, .F. ) ;
#1785=CARTESIAN_POINT ( 'NONE',  ( 27.00000000000000000, 43.00000000000000000, 11.99999999999999645 ) ) ;
#1788=LINE ( 'NONE', #2568, #7083 ) ;
#1789=VECTOR ( 'NONE', #5153, 1000.000000000000000 ) ;
#1790=ORIENTED_EDGE ( 'NONE', *, *, #6654, .F. ) ;
#1791=( BOUNDED_CURVE ( )  B_SPLINE_CURVE ( 3, ( #7370, #2997, #5112, #7273 ),
 .UNSPECIFIED., .F., .F. ) 
 B_SPLINE_CURVE_WITH_KNOTS ( ( 4, 4 ),
 ( 0.000000000000000000, 0.4772783968222097384 ),
 .UNSPECIFIED. ) 
 CURVE ( )  GEOMETRIC_REPRESENTATION_ITEM ( )  RATIONAL_B_SPLINE_CURVE ( ( 1.000000000000000000, 0.9811070276743185659, 0.9811070276743185659, 1.000000000000000000 ) ) 
 REPRESENTATION_ITEM ( '' )  );
#1798=CIRCLE ( 'NONE', #7321, 7.250000000000002665 ) ;
#1799=DIRECTION ( 'NONE',  ( -1.000000000000000000, 0.000000000000000000, 0.000000000000000000 ) ) ;
#1807=AXIS2_PLACEMENT_3D ( 'NONE', #9210, #8502, #2649 ) ;
#1808=ORIENTED_EDGE ( 'NONE', *, *, #952, .T. ) ;
#1809=VERTEX_POINT ( 'NONE', #5575 ) ;
#1816=CARTESIAN_POINT ( 'NONE',  ( 26.21170834203226718, -53.97171801779368394, -2.612255525622730001 ) ) ;
#1818=CARTESIAN_POINT ( 'NONE',  ( 52.86930915046634993, -28.38475884032111907, -81.18159060786260284 ) ) ;
#1820=FACE_OUTER_BOUND ( 'NONE', #211, .T. ) ;
#1821=EDGE_LOOP ( 'NONE', ( #6919, #5503 ) ) ;
#1826=LINE ( 'NONE', #4616, #7164 ) ;
#1828=CARTESIAN_POINT ( 'NONE',  ( -37.00000000000000000, 30.00000000000000000, -95.00000000000000000 ) ) ;
#1832=VERTEX_POINT ( 'NONE', #6437 ) ;
#1834=CARTESIAN_POINT ( 'NONE',  ( -27.00000000000000000, 43.00000000000000000, 11.99999999999999645 ) ) ;
#1842=AXIS2_PLACEMENT_3D ( 'NONE', #4187, #7112, #3459 ) ;
#1843=CARTESIAN_POINT ( 'NONE',  ( 48.15955140082798636, -36.58521010404105311, -10.14640895491553962 ) ) ;
#1848=EDGE_CURVE ( 'NONE', #7733, #3876, #6726, .T. ) ;
#1855=CARTESIAN_POINT ( 'NONE',  ( -43.18827341296425715, 42.33902489539482872, -7.653089211995568242 ) ) ;
#1859=FACE_OUTER_BOUND ( 'NONE', #4732, .T. ) ;
#1862=PLANE ( 'NONE',  #3273 ) ;
#1869=ORIENTED_EDGE ( 'NONE', *, *, #349, .F. ) ;
#1876=CARTESIAN_POINT ( 'NONE',  ( -51.96152422706632734, 30.00000000000000000, -80.85015119857381194 ) ) ;
#1881=ORIENTED_EDGE ( 'NONE', *, *, #3809, .T. ) ;
#1883=LINE ( 'NONE', #7747, #4871 ) ;
#1903=CARTESIAN_POINT ( 'NONE',  ( 27.00000000000000000, -43.00000000000000000, -25.00000000000000000 ) ) ;
#1907=AXIS2_PLACEMENT_3D ( 'NONE', #5134, #1477, #2304 ) ;
#1908=CARTESIAN_POINT ( 'NONE',  ( 27.00000000000000000, 43.00000000000000000, 25.00000000000000000 ) ) ;
#1913=AXIS2_PLACEMENT_3D ( 'NONE', #6620, #1376, #3584 ) ;
#1915=DIRECTION ( 'NONE',  ( -0.7071067811865470176, 0.000000000000000000, 0.7071067811865481278 ) ) ;
#1926=ORIENTED_EDGE ( 'NONE', *, *, #156, .T. ) ;
#1927=ORIENTED_EDGE ( 'NONE', *, *, #2427, .T. ) ;
#1938=VERTEX_POINT ( 'NONE', #7280 ) ;
#1943=CARTESIAN_POINT ( 'NONE',  ( 53.29490495164537833, -48.67545040036924320, -60.28901569369803326 ) ) ;
#1945=VECTOR ( 'NONE', #2086, 999.9999999999998863 ) ;
#1950=ORIENTED_EDGE ( 'NONE', *, *, #7589, .T. ) ;
#1958=DIRECTION ( 'NONE',  ( -1.000000000000000000, 0.000000000000000000, 0.000000000000000000 ) ) ;
#1960=AXIS2_PLACEMENT_3D ( 'NONE', #8220, #772, #730 ) ;
#1965=CIRCLE ( 'NONE', #7475, 3.000000000000002665 ) ;
#1966=DIRECTION ( 'NONE',  ( -1.000000000000000000, 0.000000000000000000, 0.000000000000000000 ) ) ;
#1968=VECTOR ( 'NONE', #6001, 1000.000000000000000 ) ;
#1970=VERTEX_POINT ( 'NONE', #3921 ) ;
#1974=VERTEX_POINT ( 'NONE', #1668 ) ;
#1975=VERTEX_POINT ( 'NONE', #8199 ) ;
#1979=CIRCLE ( 'NONE', #4894, 60.00000000000000000 ) ;
#1984=DIRECTION ( 'NONE',  ( 0.000000000000000000, 0.000000000000000000, 1.000000000000000000 ) ) ;
#1987=LINE ( 'NONE', #4911, #262 ) ;
#2011=ADVANCED_FACE ( 'NONE', ( #986 ), #134, .F. ) ;
#2015=DIRECTION ( 'NONE',  ( -1.000000000000000000, 0.000000000000000000, 0.000000000000000000 ) ) ;
#2016=FACE_BOUND ( 'NONE', #2160, .T. ) ;
#2018=VECTOR ( 'NONE', #2991, 1000.000000000000000 ) ;
#2026=CARTESIAN_POINT ( 'NONE',  ( 50.79490495164537833, -12.50000000000000000, -100.0000000000000000 ) ) ;
#2027=FACE_OUTER_BOUND ( 'NONE', #5263, .T. ) ;
#2036=AXIS2_PLACEMENT_3D ( 'NONE', #7883, #8558, #484 ) ;
#2042=VECTOR ( 'NONE', #2652, 1000.000000000000000 ) ;
#2051=CARTESIAN_POINT ( 'NONE',  ( 62.09859669818811767, -30.00000000000000000, -66.51416582715444292 ) ) ;
#2057=ORIENTED_EDGE ( 'NONE', *, *, #5015, .T. ) ;
#2060=CIRCLE ( 'NONE', #4512, 11.00000000000000711 ) ;
#2067=ORIENTED_EDGE ( 'NONE', *, *, #4257, .F. ) ;
#2068=EDGE_CURVE ( 'NONE', #3926, #5660, #7414, .T. ) ;
#2069=DIRECTION ( 'NONE',  ( 0.000000000000000000, 0.000000000000000000, 1.000000000000000000 ) ) ;
#2073=CARTESIAN_POINT ( 'NONE',  ( 60.00000000000000000, -15.90990257669733943, -54.09009742330271564 ) ) ;
#2076=ORIENTED_EDGE ( 'NONE', *, *, #8303, .T. ) ;
#2077=CARTESIAN_POINT ( 'NONE',  ( 60.00000000000000000, -15.90990257669733943, -82.90990257669729147 ) ) ;
#2078=ORIENTED_EDGE ( 'NONE', *, *, #6483, .F. ) ;
#2081=CARTESIAN_POINT ( 'NONE',  ( 26.21170834203226718, -53.97171801779368394, -2.612255525622730001 ) ) ;
#2084=ORIENTED_EDGE ( 'NONE', *, *, #9254, .F. ) ;
#2085=EDGE_LOOP ( 'NONE', ( #2839, #8017, #2157, #2479 ) ) ;
#2086=DIRECTION ( 'NONE',  ( 0.000000000000000000, -0.7071067811865479058, 0.7071067811865472397 ) ) ;
#2087=ORIENTED_EDGE ( 'NONE', *, *, #3950, .T. ) ;
#2089=FACE_OUTER_BOUND ( 'NONE', #7476, .T. ) ;
#2092=AXIS2_PLACEMENT_3D ( 'NONE', #232, #9061, #4746 ) ;
#2093=FACE_BOUND ( 'NONE', #3877, .T. ) ;
#2097=EDGE_LOOP ( 'NONE', ( #9390, #425, #6461, #3010 ) ) ;
#2098=ORIENTED_EDGE ( 'NONE', *, *, #4434, .F. ) ;
#2099=VECTOR ( 'NONE', #7500, 1000.000000000000000 ) ;
#2102=AXIS2_PLACEMENT_3D ( 'NONE', #7684, #9113, #6057 ) ;
#2104=CARTESIAN_POINT ( 'NONE',  ( 60.00000000000000000, 15.90990257669733943, -88.90990257669730568 ) ) ;
#2105=VECTOR ( 'NONE', #6829, 1000.000000000000000 ) ;
#2110=ORIENTED_EDGE ( 'NONE', *, *, #4596, .F. ) ;
#2111=ORIENTED_EDGE ( 'NONE', *, *, #135, .F. ) ;
#2123=VECTOR ( 'NONE', #4164, 1000.000000000000000 ) ;
#2125=EDGE_CURVE ( 'NONE', #18, #2310, #5513, .T. ) ;
#2126=DIRECTION ( 'NONE',  ( 0.000000000000000000, 0.7071067811865479058, -0.7071067811865472397 ) ) ;
#2130=CARTESIAN_POINT ( 'NONE',  ( 16.00000000000000000, 21.00000000000000000, -16.89999999999999858 ) ) ;
#2132=AXIS2_PLACEMENT_3D ( 'NONE', #62, #8132, #8840 ) ;
#2144=CARTESIAN_POINT ( 'NONE',  ( 27.00000000000000000, 43.00000000000000000, -25.00000000000000000 ) ) ;
#2145=LINE ( 'NONE', #2051, #2478 ) ;
#2146=CARTESIAN_POINT ( 'NONE',  ( -53.29490495164537833, -15.90990257669733943, -57.09009742330271564 ) ) ;
#2148=EDGE_LOOP ( 'NONE', ( #3204, #7272, #8999, #324, #1275, #1176 ) ) ;
#2149=EDGE_LOOP ( 'NONE', ( #5067, #8555, #846, #1075 ) ) ;
#2152=DIRECTION ( 'NONE',  ( 0.000000000000000000, 1.000000000000000000, 0.000000000000000000 ) ) ;
#2154=FACE_BOUND ( 'NONE', #8202, .T. ) ;
#2156=CARTESIAN_POINT ( 'NONE',  ( -37.00000000000000711, -3.673940397442057600E-15, -55.00000000000000711 ) ) ;
#2157=ORIENTED_EDGE ( 'NONE', *, *, #3307, .F. ) ;
#2160=EDGE_LOOP ( 'NONE', ( #5099, #2087 ) ) ;
#2169=LINE ( 'NONE', #636, #5333 ) ;
#2179=EDGE_LOOP ( 'NONE', ( #4949, #30, #4923, #6668 ) ) ;
#2184=CYLINDRICAL_SURFACE ( 'NONE', #289, 15.00000000000000000 ) ;
#2187=DIRECTION ( 'NONE',  ( 0.000000000000000000, 0.7071067811865477948, -0.7071067811865473507 ) ) ;
#2194=ORIENTED_EDGE ( 'NONE', *, *, #2923, .T. ) ;
#2195=VERTEX_POINT ( 'NONE', #6288 ) ;
#2196=DIRECTION ( 'NONE',  ( 0.000000000000000000, -0.7071067811865479058, 0.7071067811865472397 ) ) ;
#2199=DIRECTION ( 'NONE',  ( -1.000000000000000000, 0.000000000000000000, 0.000000000000000000 ) ) ;
#2200=PLANE ( 'NONE',  #1907 ) ;
#2206=ORIENTED_EDGE ( 'NONE', *, *, #9101, .T. ) ;
#2207=AXIS2_PLACEMENT_3D ( 'NONE', #6872, #374, #332 ) ;
#2209=DIRECTION ( 'NONE',  ( 0.000000000000000000, 1.000000000000000000, 0.000000000000000000 ) ) ;
#2210=CIRCLE ( 'NONE', #1441, 11.00000000000000711 ) ;
#2213=PLANE ( 'NONE',  #2601 ) ;
#2226=EDGE_LOOP ( 'NONE', ( #2710, #3476, #9215, #7680 ) ) ;
#2228=CARTESIAN_POINT ( 'NONE',  ( -51.96152422706632024, -30.00000000000000000, -13.00000000000000000 ) ) ;
#2232=AXIS2_PLACEMENT_3D ( 'NONE', #4569, #6114, #1634 ) ;
#2233=CARTESIAN_POINT ( 'NONE',  ( 60.00000000000000000, -30.00000000000000000, -30.00000000000000000 ) ) ;
#2235=DIRECTION ( 'NONE',  ( -0.000000000000000000, -0.000000000000000000, -1.000000000000000000 ) ) ;
#2238=ORIENTED_EDGE ( 'NONE', *, *, #731, .F. ) ;
#2239=ADVANCED_FACE ( 'NONE', ( #3083 ), #3132, .F. ) ;
#2242=DIRECTION ( 'NONE',  ( 0.000000000000000000, 0.000000000000000000, 1.000000000000000000 ) ) ;
#2243=DIRECTION ( 'NONE',  ( -1.000000000000000000, 0.000000000000000000, 0.000000000000000000 ) ) ;
#2244=ADVANCED_FACE ( 'NONE', ( #6746 ), #163, .F. ) ;
#2251=DIRECTION ( 'NONE',  ( -1.000000000000000000, 0.000000000000000000, -0.000000000000000000 ) ) ;
#2253=ORIENTED_EDGE ( 'NONE', *, *, #8813, .T. ) ;
#2258=ORIENTED_EDGE ( 'NONE', *, *, #5662, .F. ) ;
#2259=EDGE_CURVE ( 'NONE', #8340, #580, #7221, .T. ) ;
#2263=DIRECTION ( 'NONE',  ( -1.000000000000000000, 0.000000000000000000, 0.000000000000000000 ) ) ;
#2267=DIRECTION ( 'NONE',  ( 0.000000000000000000, 0.000000000000000000, -1.000000000000000000 ) ) ;
#2269=CIRCLE ( 'NONE', #7790, 3.000000000000002665 ) ;
#2270=CARTESIAN_POINT ( 'NONE',  ( -26.21170834203230982, 53.97171801779368394, -0.5000000000000038858 ) ) ;
#2277=CIRCLE ( 'NONE', #9324, 7.250000000000002665 ) ;
#2278=CARTESIAN_POINT ( 'NONE',  ( 60.00000000000000000, -3.673940397442057600E-15, -70.00000000000000000 ) ) ;
#2279=AXIS2_PLACEMENT_3D ( 'NONE', #3372, #6355, #1298 ) ;
#2281=ORIENTED_EDGE ( 'NONE', *, *, #7530, .F. ) ;
#2282=EDGE_LOOP ( 'NONE', ( #8804, #7900, #4058, #5658, #9326, #1264 ) ) ;
#2286=VECTOR ( 'NONE', #3724, 1000.000000000000000 ) ;
#2299=LINE ( 'NONE', #3785, #1191 ) ;
#2301=CIRCLE ( 'NONE', #5989, 3.000000000000002665 ) ;
#2304=DIRECTION ( 'NONE',  ( 0.000000000000000000, 0.000000000000000000, -1.000000000000000000 ) ) ;
#2308=PLANE ( 'NONE',  #876 ) ;
#2310=VERTEX_POINT ( 'NONE', #4521 ) ;
#2312=FACE_OUTER_BOUND ( 'NONE', #4683, .T. ) ;
#2318=FACE_OUTER_BOUND ( 'NONE', #6956, .T. ) ;
#2319=CARTESIAN_POINT ( 'NONE',  ( 60.00000000000000000, 15.90990257669733943, -88.90990257669730568 ) ) ;
#2323=VERTEX_POINT ( 'NONE', #4720 ) ;
#2330=CARTESIAN_POINT ( 'NONE',  ( 60.00000000000000000, -15.90990257669733943, -54.09009742330271564 ) ) ;
#2332=VECTOR ( 'NONE', #6653, 1000.000000000000114 ) ;
#2335=ORIENTED_EDGE ( 'NONE', *, *, #3834, .F. ) ;
#2336=DIRECTION ( 'NONE',  ( 0.000000000000000000, 0.000000000000000000, -1.000000000000000000 ) ) ;
#2340=DIRECTION ( 'NONE',  ( 1.000000000000000000, -0.000000000000000000, -0.000000000000000000 ) ) ;
#2342=CARTESIAN_POINT ( 'NONE',  ( 60.00000000000000000, 15.90990257669733943, -54.09009742330271564 ) ) ;
#2344=CARTESIAN_POINT ( 'NONE',  ( 27.00000000000000000, 43.00000000000000000, 11.99999999999999645 ) ) ;
#2349=ORIENTED_EDGE ( 'NONE', *, *, #932, .F. ) ;
#2352=ADVANCED_FACE ( 'NONE', ( #7740 ), #4806, .F. ) ;
#2353=CIRCLE ( 'NONE', #7250, 15.00000000000000000 ) ;
#2355=FACE_BOUND ( 'NONE', #6160, .T. ) ;
#2359=VECTOR ( 'NONE', #9212, 1000.000000000000000 ) ;
#2361=LINE ( 'NONE', #2409, #5318 ) ;
#2362=( BOUNDED_CURVE ( )  B_SPLINE_CURVE ( 3, ( #1361, #9382, #4155, #8574 ),
 .UNSPECIFIED., .F., .T. ) 
 B_SPLINE_CURVE_WITH_KNOTS ( ( 4, 4 ),
 ( 4.334691002005214955, 4.712388980384689674 ),
 .UNSPECIFIED. ) 
 CURVE ( )  GEOMETRIC_REPRESENTATION_ITEM ( )  RATIONAL_B_SPLINE_CURVE ( ( 1.000000000000000000, 0.9881473088045074071, 0.9881473088045074071, 1.000000000000000000 ) ) 
 REPRESENTATION_ITEM ( '' )  );
#2364=DIRECTION ( 'NONE',  ( -1.000000000000000000, 0.000000000000000000, 0.000000000000000000 ) ) ;
#2367=PLANE ( 'NONE',  #6747 ) ;
#2368=LINE ( 'NONE', #2319, #2873 ) ;
#2372=VERTEX_POINT ( 'NONE', #3898 ) ;
#2374=ORIENTED_EDGE ( 'NONE', *, *, #4252, .F. ) ;
#2375=FACE_OUTER_BOUND ( 'NONE', #2282, .T. ) ;
#2386=DIRECTION ( 'NONE',  ( -1.000000000000000000, 0.000000000000000000, 0.000000000000000000 ) ) ;
#2392=FACE_OUTER_BOUND ( 'NONE', #7392, .T. ) ;
#2399=VERTEX_POINT ( 'NONE', #3176 ) ;
#2400=PLANE ( 'NONE',  #403 ) ;
#2403=UNCERTAINTY_MEASURE_WITH_UNIT (LENGTH_MEASURE( 1.000000000000000082E-05 ), #1011, 'distance_accuracy_value', 'NONE');
#2409=CARTESIAN_POINT ( 'NONE',  ( 38.00000000000000000, 43.00000000000000000, 11.99999999999999645 ) ) ;
#2417=ORIENTED_EDGE ( 'NONE', *, *, #4826, .T. ) ;
#2421=DIRECTION ( 'NONE',  ( 0.000000000000000000, 1.000000000000000000, 0.000000000000000000 ) ) ;
#2425=DIRECTION ( 'NONE',  ( -1.000000000000000000, 0.000000000000000000, 0.000000000000000000 ) ) ;
#2427=EDGE_CURVE ( 'NONE', #8884, #7524, #8314, .T. ) ;
#2428=DIRECTION ( 'NONE',  ( -1.000000000000000000, 0.000000000000000000, 0.000000000000000000 ) ) ;
#2431=ORIENTED_EDGE ( 'NONE', *, *, #7296, .T. ) ;
#2435=ORIENTED_EDGE ( 'NONE', *, *, #7764, .T. ) ;
#2438=CARTESIAN_POINT ( 'NONE',  ( -53.29490495164537833, -15.90990257669733943, -54.09009742330271564 ) ) ;
#2439=LINE ( 'NONE', #3197, #1420 ) ;
#2444=PLANE ( 'NONE',  #5337 ) ;
#2446=ADVANCED_FACE ( 'NONE', ( #3999 ), #7021, .F. ) ;
#2447=ORIENTED_EDGE ( 'NONE', *, *, #8229, .T. ) ;
#2449=DIRECTION ( 'NONE',  ( -1.000000000000000000, 0.000000000000000000, 0.000000000000000000 ) ) ;
#2450=VECTOR ( 'NONE', #1412, 1000.000000000000114 ) ;
#2451=ORIENTED_EDGE ( 'NONE', *, *, #5657, .F. ) ;
#2452=EDGE_CURVE ( 'NONE', #8147, #6932, #7920, .T. ) ;
#2458=DIRECTION ( 'NONE',  ( -1.000000000000000000, 0.000000000000000000, 0.000000000000000000 ) ) ;
#2464=FACE_OUTER_BOUND ( 'NONE', #8608, .T. ) ;
#2466=FACE_OUTER_BOUND ( 'NONE', #9297, .T. ) ;
#2472=EDGE_LOOP ( 'NONE', ( #3067, #4722, #5397, #1716 ) ) ;
#2473=CARTESIAN_POINT ( 'NONE',  ( -37.00000000000000000, -21.98223304703364889, -86.98223304703364533 ) ) ;
#2477=CARTESIAN_POINT ( 'NONE',  ( -38.00000000000000711, -43.00000000000000000, -7.366666666666667140 ) ) ;
#2478=VECTOR ( 'NONE', #5075, 1000.000000000000000 ) ;
#2479=ORIENTED_EDGE ( 'NONE', *, *, #3239, .F. ) ;
#2481=VERTEX_POINT ( 'NONE', #8550 ) ;
#2483=ORIENTED_EDGE ( 'NONE', *, *, #2543, .F. ) ;
#2486=CARTESIAN_POINT ( 'NONE',  ( -37.00000000000000000, 30.00000000000000000, -78.96446609406727646 ) ) ;
#2503=VERTEX_POINT ( 'NONE', #521 ) ;
#2519=CYLINDRICAL_SURFACE ( 'NONE', #1400, 11.00000000000000000 ) ;
#2523=VERTEX_POINT ( 'NONE', #1283 ) ;
#2525=CARTESIAN_POINT ( 'NONE',  ( -52.86930915046636414, -28.38475884032111196, -81.18159060786256020 ) ) ;
#2526=FACE_OUTER_BOUND ( 'NONE', #8135, .T. ) ;
#2530=VECTOR ( 'NONE', #545, 1000.000000000000000 ) ;
#2533=EDGE_CURVE ( 'NONE', #6932, #3553, #1197, .T. ) ;
#2535=ORIENTED_EDGE ( 'NONE', *, *, #2941, .T. ) ;
#2543=EDGE_CURVE ( 'NONE', #7343, #1832, #477, .T. ) ;
#2546=CARTESIAN_POINT ( 'NONE',  ( 60.00000000000000000, 15.90990257669733943, -85.90990257669729147 ) ) ;
#2548=ORIENTED_EDGE ( 'NONE', *, *, #331, .T. ) ;
#2549=ADVANCED_FACE ( 'NONE', ( #2016, #1239 ), #7063, .T. ) ;
#2551=AXIS2_PLACEMENT_3D ( 'NONE', #9049, #7463, #4639 ) ;
#2553=CARTESIAN_POINT ( 'NONE',  ( 0.000000000000000000, 0.000000000000000000, 25.00000000000000000 ) ) ;
#2561=CARTESIAN_POINT ( 'NONE',  ( -37.00000000000000000, -30.00000000000000000, -95.00000000000000000 ) ) ;
#2568=CARTESIAN_POINT ( 'NONE',  ( 39.50000000000000000, 29.99999999999999645, -82.50000000000000000 ) ) ;
#2571=VECTOR ( 'NONE', #867, 1000.000000000000000 ) ;
#2574=VERTEX_POINT ( 'NONE', #4220 ) ;
#2579=LINE ( 'NONE', #3976, #26 ) ;
#2587=ORIENTED_EDGE ( 'NONE', *, *, #4299, .F. ) ;
#2589=CARTESIAN_POINT ( 'NONE',  ( 19.74999999999999645, 43.00000000000000000, 25.00000000000000000 ) ) ;
#2595=VECTOR ( 'NONE', #935, 1000.000000000000000 ) ;
#2597=ORIENTED_EDGE ( 'NONE', *, *, #7344, .T. ) ;
#2598=CIRCLE ( 'NONE', #3520, 3.000000000000002665 ) ;
#2601=AXIS2_PLACEMENT_3D ( 'NONE', #160, #3082, #5146 ) ;
#2603=EDGE_CURVE ( 'NONE', #7596, #4808, #1431, .T. ) ;
#2610=PLANE ( 'NONE',  #5341 ) ;
#2613=CYLINDRICAL_SURFACE ( 'NONE', #5650, 11.00000000000000711 ) ;
#2615=CIRCLE ( 'NONE', #1675, 11.00000000000000711 ) ;
#2618=ADVANCED_FACE ( 'NONE', ( #5955 ), #712, .T. ) ;
#2624=EDGE_CURVE ( 'NONE', #6868, #1832, #4267, .T. ) ;
#2628=DIRECTION ( 'NONE',  ( 1.000000000000000000, -0.000000000000000000, -0.000000000000000000 ) ) ;
#2631=ORIENTED_EDGE ( 'NONE', *, *, #9056, .F. ) ;
#2633=CARTESIAN_POINT ( 'NONE',  ( -15.99999999999999645, 43.00000000000000000, -7.366666666666667140 ) ) ;
#2637=DIRECTION ( 'NONE',  ( 0.000000000000000000, 0.000000000000000000, 1.000000000000000000 ) ) ;
#2639=FACE_OUTER_BOUND ( 'NONE', #6449, .T. ) ;
#2640=CARTESIAN_POINT ( 'NONE',  ( 26.21170834203230982, 53.97171801779368394, -0.5000000000000038858 ) ) ;
#2646=AXIS2_PLACEMENT_3D ( 'NONE', #2330, #5882, #2945 ) ;
#2649=DIRECTION ( 'NONE',  ( 0.000000000000000000, 0.000000000000000000, -1.000000000000000000 ) ) ;
#2650=AXIS2_PLACEMENT_3D ( 'NONE', #3704, #4517, #6786 ) ;
#2652=DIRECTION ( 'NONE',  ( -0.000000000000000000, -0.000000000000000000, -1.000000000000000000 ) ) ;
#2655=CIRCLE ( 'NONE', #6337, 60.00000000000000000 ) ;
#2660=LINE ( 'NONE', #4859, #5017 ) ;
#2662=CARTESIAN_POINT ( 'NONE',  ( -60.00000000000000000, -30.00000000000000000, -13.00000000000000000 ) ) ;
#2664=CARTESIAN_POINT ( 'NONE',  ( -37.00000000000000711, -15.90990257669733943, -57.09009742330271564 ) ) ;
#2665=ADVANCED_FACE ( 'NONE', ( #7338, #2, #4506, #8738, #8881, #2154 ), #2200, .T. ) ;
#2673=DIRECTION ( 'NONE',  ( 0.000000000000000000, 0.000000000000000000, -1.000000000000000000 ) ) ;
#2674=CARTESIAN_POINT ( 'NONE',  ( 60.00000000000000000, 15.90990257669733943, -85.90990257669729147 ) ) ;
#2676=ORIENTED_EDGE ( 'NONE', *, *, #5228, .F. ) ;
#2677=VERTEX_POINT ( 'NONE', #8207 ) ;
#2678=DIRECTION ( 'NONE',  ( -0.000000000000000000, -0.000000000000000000, 1.000000000000000000 ) ) ;
#2681=CARTESIAN_POINT ( 'NONE',  ( -37.00000000000000000, -30.00000000000000000, -95.00000000000000000 ) ) ;
#2689=CIRCLE ( 'NONE', #1292, 3.000000000000002665 ) ;
#2690=VERTEX_POINT ( 'NONE', #5231 ) ;
#2696=ORIENTED_EDGE ( 'NONE', *, *, #135, .T. ) ;
#2698=ORIENTED_EDGE ( 'NONE', *, *, #4937, .T. ) ;
#2701=CARTESIAN_POINT ( 'NONE',  ( -38.00000000000000711, -20.99999999999999289, -16.89999999999999858 ) ) ;
#2704=CARTESIAN_POINT ( 'NONE',  ( -37.00000000000000711, -15.90990257669733943, -54.09009742330271564 ) ) ;
#2710=ORIENTED_EDGE ( 'NONE', *, *, #5371, .F. ) ;
#2714=ADVANCED_FACE ( 'NONE', ( #8120, #1527, #7387, #2355, #6731, #149 ), #1050, .T. ) ;
#2715=AXIS2_PLACEMENT_3D ( 'NONE', #7213, #6554, #8753 ) ;
#2717=EDGE_CURVE ( 'NONE', #6270, #4692, #4577, .T. ) ;
#2718=DIRECTION ( 'NONE',  ( -0.7071067811865426878, 0.000000000000000000, -0.7071067811865524577 ) ) ;
#2719=EDGE_CURVE ( 'NONE', #6045, #7524, #3900, .T. ) ;
#2729=DIRECTION ( 'NONE',  ( -1.000000000000000000, 0.000000000000000000, 0.000000000000000000 ) ) ;
#2738=PLANE ( 'NONE',  #122 ) ;
#2740=ORIENTED_EDGE ( 'NONE', *, *, #553, .T. ) ;
#2747=CARTESIAN_POINT ( 'NONE',  ( -58.90150666944372659, 9.142135623730833771, -91.89339828220165884 ) ) ;
#2749=EDGE_LOOP ( 'NONE', ( #2898, #7997 ) ) ;
#2757=DIRECTION ( 'NONE',  ( 0.000000000000000000, -0.7071067811865473507, -0.7071067811865477948 ) ) ;
#2767=DIRECTION ( 'NONE',  ( 1.000000000000000000, 0.000000000000000000, 0.000000000000000000 ) ) ;
#2771=ORIENTED_EDGE ( 'NONE', *, *, #21, .T. ) ;
#2775=DIRECTION ( 'NONE',  ( 1.000000000000000000, 0.000000000000000000, 0.000000000000000000 ) ) ;
#2782=ADVANCED_FACE ( 'NONE', ( #4610 ), #1768, .F. ) ;
#2783=EDGE_LOOP ( 'NONE', ( #7771, #7752, #7346, #5312, #2111 ) ) ;
#2787=CARTESIAN_POINT ( 'NONE',  ( 19.74999999999999645, -43.00000000000000000, 11.99999999999999645 ) ) ;
#2789=LINE ( 'NONE', #5724, #4409 ) ;
#2791=ORIENTED_EDGE ( 'NONE', *, *, #4233, .F. ) ;
#2792=EDGE_LOOP ( 'NONE', ( #8710, #1524, #8498, #123, #5111 ) ) ;
#2794=EDGE_LOOP ( 'NONE', ( #2110, #6691, #8786, #3108 ) ) ;
#2796=AXIS2_PLACEMENT_3D ( 'NONE', #5639, #8562, #1984 ) ;
#2802=CARTESIAN_POINT ( 'NONE',  ( -50.79490495164537833, -30.00000000000000355, -82.50000000000001421 ) ) ;
#2804=DIRECTION ( 'NONE',  ( -0.000000000000000000, -0.000000000000000000, -1.000000000000000000 ) ) ;
#2805=VECTOR ( 'NONE', #2421, 1000.000000000000000 ) ;
#2807=EDGE_CURVE ( 'NONE', #4540, #95, #5755, .T. ) ;
#2810=EDGE_CURVE ( 'NONE', #3864, #2503, #6978, .T. ) ;
#2816=ORIENTED_EDGE ( 'NONE', *, *, #3657, .T. ) ;
#2820=DIRECTION ( 'NONE',  ( -1.000000000000000000, 0.000000000000000000, 0.000000000000000000 ) ) ;
#2823=EDGE_CURVE ( 'NONE', #5944, #3926, #6201, .T. ) ;
#2824=LINE ( 'NONE', #4268, #9111 ) ;
#2826=VERTEX_POINT ( 'NONE', #9112 ) ;
#2830=ADVANCED_FACE ( 'NONE', ( #8305, #4659, #7582, #4755, #998 ), #4033, .T. ) ;
#2836=EDGE_CURVE ( 'NONE', #3553, #5088, #2824, .T. ) ;
#2838=ORIENTED_EDGE ( 'NONE', *, *, #5772, .F. ) ;
#2839=ORIENTED_EDGE ( 'NONE', *, *, #8643, .F. ) ;
#2840=ORIENTED_EDGE ( 'NONE', *, *, #3633, .F. ) ;
#2844=LINE ( 'NONE', #2662, #9179 ) ;
#2845=AXIS2_PLACEMENT_3D ( 'NONE', #7721, #1131, #7619 ) ;
#2847=DIRECTION ( 'NONE',  ( -0.000000000000000000, 1.000000000000000000, 0.000000000000000000 ) ) ;
#2852=CARTESIAN_POINT ( 'NONE',  ( 20.14434505884620918, 53.53579249963522102, -2.801156583491397623 ) ) ;
#2857=CARTESIAN_POINT ( 'NONE',  ( 43.18827341296426425, 42.33902489539482872, -7.653089211995569130 ) ) ;
#2865=CYLINDRICAL_SURFACE ( 'NONE', #1472, 3.000000000000002665 ) ;
#2870=VECTOR ( 'NONE', #2900, 1000.000000000000114 ) ;
#2873=VECTOR ( 'NONE', #6745, 1000.000000000000000 ) ;
#2874=CARTESIAN_POINT ( 'NONE',  ( 53.29490495164537833, 27.56180520566613268, -41.61356529332876875 ) ) ;
#2877=AXIS2_PLACEMENT_3D ( 'NONE', #4144, #6403, #486 ) ;
#2879=DIRECTION ( 'NONE',  ( 0.000000000000000000, -0.7071067811865472397, -0.7071067811865479058 ) ) ;
#2888=EDGE_CURVE ( 'NONE', #7697, #7845, #7821, .T. ) ;
#2889=CYLINDRICAL_SURFACE ( 'NONE', #3188, 11.00000000000000711 ) ;
#2892=CARTESIAN_POINT ( 'NONE',  ( 53.29490495164537833, -48.67545040036925030, -60.28901569369804037 ) ) ;
#2898=ORIENTED_EDGE ( 'NONE', *, *, #8911, .T. ) ;
#2900=DIRECTION ( 'NONE',  ( -0.5773502691896249539, 0.5773502691896263972, -0.5773502691896258421 ) ) ;
#2903=DIRECTION ( 'NONE',  ( 1.000000000000000000, -0.000000000000000000, -0.000000000000000000 ) ) ;
#2905=VERTEX_POINT ( 'NONE', #5619 ) ;
#2910=FACE_OUTER_BOUND ( 'NONE', #3235, .T. ) ;
#2911=CARTESIAN_POINT ( 'NONE',  ( -39.50000000000000711, -30.00000000000000355, -82.50000000000001421 ) ) ;
#2915=VERTEX_POINT ( 'NONE', #4796 ) ;
#2923=EDGE_CURVE ( 'NONE', #9426, #955, #2060, .T. ) ;
#2927=CIRCLE ( 'NONE', #8304, 7.250000000000002665 ) ;
#2933=CARTESIAN_POINT ( 'NONE',  ( -37.00000000000000000, -8.017766952966344007, -116.9822330470336453 ) ) ;
#2934=FACE_OUTER_BOUND ( 'NONE', #5212, .T. ) ;
#2941=EDGE_CURVE ( 'NONE', #4363, #7585, #7866, .T. ) ;
#2945=DIRECTION ( 'NONE',  ( 0.000000000000000000, 0.000000000000000000, 1.000000000000000000 ) ) ;
#2946=ADVANCED_FACE ( 'NONE', ( #6299 ), #4889, .F. ) ;
#2948=ORIENTED_EDGE ( 'NONE', *, *, #8637, .F. ) ;
#2951=ORIENTED_EDGE ( 'NONE', *, *, #8563, .T. ) ;
#2956=PLANE ( 'NONE',  #5538 ) ;
#2963=ORIENTED_EDGE ( 'NONE', *, *, #5662, .T. ) ;
#2965=CARTESIAN_POINT ( 'NONE',  ( -37.00000000000000711, -1.836970198721028011E-15, -85.00000000000000000 ) ) ;
#2968=CARTESIAN_POINT ( 'NONE',  ( 60.00000000000000000, -15.90990257669733943, -85.90990257669729147 ) ) ;
#2969=CARTESIAN_POINT ( 'NONE',  ( 37.73845885098648267, -45.76160744848121453, -6.169970105658134862 ) ) ;
#2971=ORIENTED_EDGE ( 'NONE', *, *, #4754, .T. ) ;
#2976=FACE_OUTER_BOUND ( 'NONE', #3768, .T. ) ;
#2980=DIRECTION ( 'NONE',  ( 0.000000000000000000, 0.000000000000000000, 1.000000000000000000 ) ) ;
#2984=ORIENTED_EDGE ( 'NONE', *, *, #7963, .F. ) ;
#2985=DIRECTION ( 'NONE',  ( -1.000000000000000000, 0.000000000000000000, -0.000000000000000000 ) ) ;
#2988=FACE_OUTER_BOUND ( 'NONE', #6451, .T. ) ;
#2990=CARTESIAN_POINT ( 'NONE',  ( -60.00000000000000000, -60.00000000000000000, 0.000000000000000000 ) ) ;
#2991=DIRECTION ( 'NONE',  ( 0.000000000000000000, 1.000000000000000000, 0.000000000000000000 ) ) ;
#2994=ORIENTED_EDGE ( 'NONE', *, *, #441, .F. ) ;
#2995=( NAMED_UNIT ( * ) PLANE_ANGLE_UNIT ( ) SI_UNIT ( $, .RADIAN. ) );
#2997=CARTESIAN_POINT ( 'NONE',  ( -60.00000000000001421, 9.637301612213114765, -29.99999999999998934 ) ) ;
#3000=FACE_BOUND ( 'NONE', #4708, .T. ) ;
#3001=ADVANCED_FACE ( 'NONE', ( #43 ), #5894, .T. ) ;
#3003=EDGE_CURVE ( 'NONE', #95, #4540, #1760, .T. ) ;
#3004=FACE_BOUND ( 'NONE', #5763, .T. ) ;
#3005=AXIS2_PLACEMENT_3D ( 'NONE', #7298, #5775, #1487 ) ;
#3010=ORIENTED_EDGE ( 'NONE', *, *, #4400, .T. ) ;
#3012=CYLINDRICAL_SURFACE ( 'NONE', #4255, 7.250000000000002665 ) ;
#3018=DIRECTION ( 'NONE',  ( 0.000000000000000000, 0.000000000000000000, -1.000000000000000000 ) ) ;
#3027=CARTESIAN_POINT ( 'NONE',  ( -27.00000000000000000, 43.00000000000000000, 11.99999999999999645 ) ) ;
#3028=( BOUNDED_CURVE ( )  B_SPLINE_CURVE ( 3, ( #3567, #685, #2130, #6506 ),
 .UNSPECIFIED., .F., .F. ) 
 B_SPLINE_CURVE_WITH_KNOTS ( ( 4, 4 ),
 ( 4.712388980384689674, 7.853981633974482790 ),
 .UNSPECIFIED. ) 
 CURVE ( )  GEOMETRIC_REPRESENTATION_ITEM ( )  RATIONAL_B_SPLINE_CURVE ( ( 1.000000000000000000, 0.3333333333333333703, 0.3333333333333333703, 1.000000000000000000 ) ) 
 REPRESENTATION_ITEM ( '' )  );
#3030=VECTOR ( 'NONE', #1334, 1000.000000000000000 ) ;
#3032=AXIS2_PLACEMENT_3D ( 'NONE', #1468, #3636, #5895 ) ;
#3036=DIRECTION ( 'NONE',  ( 0.000000000000000000, 0.000000000000000000, -1.000000000000000000 ) ) ;
#3037=EDGE_LOOP ( 'NONE', ( #6137, #5186, #3668, #1761 ) ) ;
#3042=CARTESIAN_POINT ( 'NONE',  ( -32.83333333333333570, -21.66666666666668206, -90.83333333333332860 ) ) ;
#3046=LINE ( 'NONE', #3142, #8160 ) ;
#3055=CYLINDRICAL_SURFACE ( 'NONE', #8726, 3.000000000000002665 ) ;
#3067=ORIENTED_EDGE ( 'NONE', *, *, #8813, .F. ) ;
#3068=DIRECTION ( 'NONE',  ( -0.000000000000000000, -0.000000000000000000, 1.000000000000000000 ) ) ;
#3082=DIRECTION ( 'NONE',  ( -0.7071067811865494601, -0.4999999999999988343, 0.4999999999999985012 ) ) ;
#3083=FACE_OUTER_BOUND ( 'NONE', #3263, .T. ) ;
#3085=ORIENTED_EDGE ( 'NONE', *, *, #4357, .T. ) ;
#3088=CARTESIAN_POINT ( 'NONE',  ( -53.29490495164537833, -30.00000000000000000, -41.61356529332876875 ) ) ;
#3089=LINE ( 'NONE', #3042, #2870 ) ;
#3098=CARTESIAN_POINT ( 'NONE',  ( 27.00000000000000000, -43.00000000000000000, 25.00000000000000000 ) ) ;
#3100=PLANE ( 'NONE',  #4555 ) ;
#3102=DIRECTION ( 'NONE',  ( -1.000000000000000000, 0.000000000000000000, 0.000000000000000000 ) ) ;
#3106=CIRCLE ( 'NONE', #4947, 15.00000000000000000 ) ;
#3108=ORIENTED_EDGE ( 'NONE', *, *, #952, .F. ) ;
#3111=ORIENTED_EDGE ( 'NONE', *, *, #6, .F. ) ;
#3112=LINE ( 'NONE', #369, #7410 ) ;
#3114=VECTOR ( 'NONE', #4688, 999.9999999999998863 ) ;
#3119=ORIENTED_EDGE ( 'NONE', *, *, #6547, .T. ) ;
#3120=VERTEX_POINT ( 'NONE', #2146 ) ;
#3123=EDGE_CURVE ( 'NONE', #4316, #3234, #5121, .T. ) ;
#3132=CYLINDRICAL_SURFACE ( 'NONE', #4195, 15.00000000000000000 ) ;
#3133=ORIENTED_EDGE ( 'NONE', *, *, #5299, .F. ) ;
#3136=CARTESIAN_POINT ( 'NONE',  ( -27.00000000000000000, -43.00000000000000000, 11.99999999999999645 ) ) ;
#3142=CARTESIAN_POINT ( 'NONE',  ( -34.25000000000000000, -43.00000000000000000, -25.00000000000000000 ) ) ;
#3144=VERTEX_POINT ( 'NONE', #6768 ) ;
#3145=AXIS2_PLACEMENT_3D ( 'NONE', #4198, #5789, #8616 ) ;
#3146=ORIENTED_EDGE ( 'NONE', *, *, #894, .F. ) ;
#3147=ORIENTED_EDGE ( 'NONE', *, *, #8411, .T. ) ;
#3158=CARTESIAN_POINT ( 'NONE',  ( 60.00000000000000000, 12.50000000000000000, -100.0000000000000000 ) ) ;
#3159=ORIENTED_EDGE ( 'NONE', *, *, #8922, .F. ) ;
#3167=ORIENTED_EDGE ( 'NONE', *, *, #7958, .T. ) ;
#3169=CARTESIAN_POINT ( 'NONE',  ( -27.00000000000000000, -43.00000000000000000, 11.99999999999999645 ) ) ;
#3171=AXIS2_PLACEMENT_3D ( 'NONE', #6186, #9095, #1799 ) ;
#3176=CARTESIAN_POINT ( 'NONE',  ( -37.00000000000000711, 15.90990257669733943, -88.90990257669730568 ) ) ;
#3179=ADVANCED_FACE ( 'NONE', ( #2392 ), #3825, .T. ) ;
#3187=DIRECTION ( 'NONE',  ( 0.000000000000000000, 0.7071067811865479058, -0.7071067811865472397 ) ) ;
#3188=AXIS2_PLACEMENT_3D ( 'NONE', #5819, #5912, #2263 ) ;
#3189=FACE_OUTER_BOUND ( 'NONE', #2226, .T. ) ;
#3190=ADVANCED_FACE ( 'NONE', ( #1160, #4644 ), #2444, .T. ) ;
#3194=ORIENTED_EDGE ( 'NONE', *, *, #4124, .T. ) ;
#3197=CARTESIAN_POINT ( 'NONE',  ( -40.05867498135627613, -15.23141075423628799, -98.05867498135629035 ) ) ;
#3199=AXIS2_PLACEMENT_3D ( 'NONE', #5615, #8537, #1958 ) ;
#3203=DIRECTION ( 'NONE',  ( 0.000000000000000000, 0.000000000000000000, 1.000000000000000000 ) ) ;
#3204=ORIENTED_EDGE ( 'NONE', *, *, #5960, .T. ) ;
#3208=ORIENTED_EDGE ( 'NONE', *, *, #7362, .F. ) ;
#3211=VERTEX_POINT ( 'NONE', #5321 ) ;
#3213=DIRECTION ( 'NONE',  ( -1.000000000000000000, 0.000000000000000000, 0.000000000000000000 ) ) ;
#3219=ADVANCED_FACE ( 'NONE', ( #4147 ), #5594, .F. ) ;
#3221=DIRECTION ( 'NONE',  ( -1.000000000000000000, 0.000000000000000000, 0.000000000000000000 ) ) ;
#3223=LINE ( 'NONE', #1828, #4479 ) ;
#3226=EDGE_LOOP ( 'NONE', ( #3119, #1301, #1255, #8020, #3597, #4445 ) ) ;
#3228=DIRECTION ( 'NONE',  ( 0.000000000000000000, 0.000000000000000000, 1.000000000000000000 ) ) ;
#3233=AXIS2_PLACEMENT_3D ( 'NONE', #225, #6663, #5271 ) ;
#3234=VERTEX_POINT ( 'NONE', #6145 ) ;
#3235=EDGE_LOOP ( 'NONE', ( #6864, #2548, #1313, #1315 ) ) ;
#3237=EDGE_LOOP ( 'NONE', ( #1066, #8967, #220, #7178 ) ) ;
#3239=EDGE_CURVE ( 'NONE', #3622, #8690, #8474, .T. ) ;
#3240=DIRECTION ( 'NONE',  ( 0.000000000000000000, 0.000000000000000000, -1.000000000000000000 ) ) ;
#3242=DIRECTION ( 'NONE',  ( -1.000000000000000000, 0.000000000000000000, 0.000000000000000000 ) ) ;
#3244=CARTESIAN_POINT ( 'NONE',  ( 51.96152422706632024, 29.99999999999999645, -12.99999999999999822 ) ) ;
#3256=CARTESIAN_POINT ( 'NONE',  ( 37.22467645238199196, 47.05659850664387278, -5.608807313787652404 ) ) ;
#3263=EDGE_LOOP ( 'NONE', ( #1340, #8260, #4635, #7293 ) ) ;
#3265=FACE_OUTER_BOUND ( 'NONE', #2792, .T. ) ;
#3268=CYLINDRICAL_SURFACE ( 'NONE', #7814, 15.00000000000000000 ) ;
#3273=AXIS2_PLACEMENT_3D ( 'NONE', #7724, #6814, #6957 ) ;
#3279=( BOUNDED_CURVE ( )  B_SPLINE_CURVE ( 3, ( #3609, #4861, #6546, #9467 ),
 .UNSPECIFIED., .F., .T. ) 
 B_SPLINE_CURVE_WITH_KNOTS ( ( 4, 4 ),
 ( 3.213317012039607956, 4.712388980384689674 ),
 .UNSPECIFIED. ) 
 CURVE ( )  GEOMETRIC_REPRESENTATION_ITEM ( )  RATIONAL_B_SPLINE_CURVE ( ( 1.000000000000000000, 0.8213367208436770373, 0.8213367208436770373, 1.000000000000000000 ) ) 
 REPRESENTATION_ITEM ( '' )  );
#3283=VERTEX_POINT ( 'NONE', #4234 ) ;
#3291=ORIENTED_EDGE ( 'NONE', *, *, #3410, .F. ) ;
#3295=ORIENTED_EDGE ( 'NONE', *, *, #4417, .F. ) ;
#3303=DIRECTION ( 'NONE',  ( 0.000000000000000000, 0.000000000000000000, 1.000000000000000000 ) ) ;
#3304=CARTESIAN_POINT ( 'NONE',  ( -38.00000000000000000, 44.39318849903271769, -6.762951650419153360 ) ) ;
#3305=ORIENTED_EDGE ( 'NONE', *, *, #2259, .F. ) ;
#3306=ORIENTED_EDGE ( 'NONE', *, *, #7386, .F. ) ;
#3307=EDGE_CURVE ( 'NONE', #8690, #55, #8794, .T. ) ;
#3312=AXIS2_PLACEMENT_3D ( 'NONE', #629, #3658, #4426 ) ;
#3314=ADVANCED_FACE ( 'NONE', ( #2934 ), #5917, .F. ) ;
#3321=VECTOR ( 'NONE', #9388, 1000.000000000000000 ) ;
#3323=CARTESIAN_POINT ( 'NONE',  ( 60.00000000000000000, -15.90990257669733943, -57.09009742330271564 ) ) ;
#3325=CIRCLE ( 'NONE', #3939, 3.000000000000002665 ) ;
#3330=ORIENTED_EDGE ( 'NONE', *, *, #932, .T. ) ;
#3333=VECTOR ( 'NONE', #7649, 1000.000000000000000 ) ;
#3337=( BOUNDED_CURVE ( )  B_SPLINE_CURVE ( 3, ( #9225, #1021, #974, #446 ),
 .UNSPECIFIED., .F., .F. ) 
 B_SPLINE_CURVE_WITH_KNOTS ( ( 4, 4 ),
 ( 4.334691002005220284, 4.712388980384689674 ),
 .UNSPECIFIED. ) 
 CURVE ( )  GEOMETRIC_REPRESENTATION_ITEM ( )  RATIONAL_B_SPLINE_CURVE ( ( 1.000000000000000000, 0.9881473088045076292, 0.9881473088045076292, 1.000000000000000000 ) ) 
 REPRESENTATION_ITEM ( '' )  );
#3347=CARTESIAN_POINT ( 'NONE',  ( 53.29490495164537833, -30.00000000000000000, -41.61356529332876875 ) ) ;
#3365=CARTESIAN_POINT ( 'NONE',  ( 34.25000000000000000, 43.00000000000000000, 25.00000000000000000 ) ) ;
#3366=DIRECTION ( 'NONE',  ( 0.7071067811865454633, 0.5000000000000012212, 0.5000000000000016653 ) ) ;
#3370=EDGE_CURVE ( 'NONE', #2826, #8754, #8081, .T. ) ;
#3371=CARTESIAN_POINT ( 'NONE',  ( 0.000000000000000000, 0.000000000000000000, 25.00000000000000000 ) ) ;
#3372=CARTESIAN_POINT ( 'NONE',  ( 53.29490495164537833, -3.673940397442057600E-15, -70.00000000000000000 ) ) ;
#3374=DIRECTION ( 'NONE',  ( 0.000000000000000000, 0.9175556253099241832, 0.3976074376343005090 ) ) ;
#3380=AXIS2_PLACEMENT_3D ( 'NONE', #2342, #3102, #5168 ) ;
#3384=VERTEX_POINT ( 'NONE', #7447 ) ;
#3386=CARTESIAN_POINT ( 'NONE',  ( 27.00000000000000000, 43.00000000000000000, 25.00000000000000000 ) ) ;
#3387=VECTOR ( 'NONE', #1404, 999.9999999999998863 ) ;
#3390=DIRECTION ( 'NONE',  ( 0.7071067811865481278, 0.000000000000000000, -0.7071067811865470176 ) ) ;
#3407=VERTEX_POINT ( 'NONE', #63 ) ;
#3408=EDGE_CURVE ( 'NONE', #313, #6124, #16, .T. ) ;
#3410=EDGE_CURVE ( 'NONE', #5804, #5944, #8397, .T. ) ;
#3413=EDGE_CURVE ( 'NONE', #2399, #3876, #2368, .T. ) ;
#3414=DIRECTION ( 'NONE',  ( 0.000000000000000000, 0.000000000000000000, -1.000000000000000000 ) ) ;
#3416=CARTESIAN_POINT ( 'NONE',  ( 53.29490495164537833, 15.90990257669733943, -82.90990257669729147 ) ) ;
#3423=LINE ( 'NONE', #8612, #964 ) ;
#3425=CARTESIAN_POINT ( 'NONE',  ( -37.00000000000000000, 13.96446609406729067, -95.00000000000000000 ) ) ;
#3428=CARTESIAN_POINT ( 'NONE',  ( 37.00000000000000000, -3.673940397442057600E-15, -55.00000000000000711 ) ) ;
#3431=ORIENTED_EDGE ( 'NONE', *, *, #892, .T. ) ;
#3432=CARTESIAN_POINT ( 'NONE',  ( -38.00000000000000711, 20.99999999999999289, -16.89999999999999858 ) ) ;
#3434=CARTESIAN_POINT ( 'NONE',  ( 20.14434505884618432, -53.53579249963522102, -2.801156583491408281 ) ) ;
#3438=CARTESIAN_POINT ( 'NONE',  ( -53.29490495164537833, 15.90990257669733943, -88.90990257669730568 ) ) ;
#3439=VECTOR ( 'NONE', #5035, 999.9999999999998863 ) ;
#3444=ORIENTED_EDGE ( 'NONE', *, *, #4829, .F. ) ;
#3449=CYLINDRICAL_SURFACE ( 'NONE', #6877, 7.250000000000002665 ) ;
#3450=PRODUCT_DEFINITION_FORMATION_WITH_SPECIFIED_SOURCE ( 'ANY', '', #5855, .NOT_KNOWN. ) ;
#3453=VERTEX_POINT ( 'NONE', #2787 ) ;
#3454=ORIENTED_EDGE ( 'NONE', *, *, #6961, .T. ) ;
#3459=DIRECTION ( 'NONE',  ( 0.000000000000000000, 0.000000000000000000, 1.000000000000000000 ) ) ;
#3470=CARTESIAN_POINT ( 'NONE',  ( 27.00000000000000000, -43.00000000000000000, 11.99999999999999645 ) ) ;
#3471=EDGE_CURVE ( 'NONE', #8884, #6290, #572, .T. ) ;
#3475=VECTOR ( 'NONE', #8739, 1000.000000000000000 ) ;
#3476=ORIENTED_EDGE ( 'NONE', *, *, #892, .F. ) ;
#3490=ORIENTED_EDGE ( 'NONE', *, *, #1752, .T. ) ;
#3493=CARTESIAN_POINT ( 'NONE',  ( -26.21170834203224231, 53.97171801779369105, -2.612255525622730001 ) ) ;
#3503=ORIENTED_EDGE ( 'NONE', *, *, #9396, .T. ) ;
#3510=ADVANCED_FACE ( 'NONE', ( #9302 ), #3689, .T. ) ;
#3511=DIRECTION ( 'NONE',  ( -1.000000000000000000, 0.000000000000000000, 0.000000000000000000 ) ) ;
#3514=VERTEX_POINT ( 'NONE', #9359 ) ;
#3515=LINE ( 'NONE', #7261, #5014 ) ;
#3518=EDGE_CURVE ( 'NONE', #2523, #3864, #8685, .T. ) ;
#3520=AXIS2_PLACEMENT_3D ( 'NONE', #676, #7442, #12 ) ;
#3522=CARTESIAN_POINT ( 'NONE',  ( -59.00000000000000000, 0.000000000000000000, 25.00000000000000000 ) ) ;
#3531=DIRECTION ( 'NONE',  ( 0.000000000000000000, 0.000000000000000000, 1.000000000000000000 ) ) ;
#3532=VECTOR ( 'NONE', #3728, 1000.000000000000000 ) ;
#3533=CARTESIAN_POINT ( 'NONE',  ( 53.29490495164537833, -15.90990257669733943, -88.90990257669730568 ) ) ;
#3539=VECTOR ( 'NONE', #7265, 1000.000000000000000 ) ;
#3543=CARTESIAN_POINT ( 'NONE',  ( 60.00000000000000000, 29.99999999999999645, -82.50000000000000000 ) ) ;
#3547=EDGE_CURVE ( 'NONE', #7512, #4808, #9449, .T. ) ;
#3548=EDGE_CURVE ( 'NONE', #1211, #8690, #5083, .T. ) ;
#3549=CARTESIAN_POINT ( 'NONE',  ( 41.99999999999999289, -30.00000000000000000, -100.0000000000000000 ) ) ;
#3553=VERTEX_POINT ( 'NONE', #4365 ) ;
#3560=DIRECTION ( 'NONE',  ( 0.000000000000000000, 0.000000000000000000, 1.000000000000000000 ) ) ;
#3561=FACE_OUTER_BOUND ( 'NONE', #2148, .T. ) ;
#3566=EDGE_LOOP ( 'NONE', ( #2238, #1881, #7050, #850, #7106, #6058, #2076, #4992, #4253, #4056, #7097, #9243 ) ) ;
#3567=CARTESIAN_POINT ( 'NONE',  ( 38.00000000000000000, 43.00000000000000000, -7.366666666666667140 ) ) ;
#3569=CARTESIAN_POINT ( 'NONE',  ( 34.25000000000000000, -43.00000000000000000, 11.99999999999999645 ) ) ;
#3571=LINE ( 'NONE', #3522, #5128 ) ;
#3573=ORIENTED_EDGE ( 'NONE', *, *, #7351, .T. ) ;
#3575=ORIENTED_EDGE ( 'NONE', *, *, #800, .T. ) ;
#3577=ORIENTED_EDGE ( 'NONE', *, *, #6534, .T. ) ;
#3580=DIRECTION ( 'NONE',  ( -0.5773502691896283956, -0.000000000000000000, 0.8164965809277242581 ) ) ;
#3583=( BOUNDED_CURVE ( )  B_SPLINE_CURVE ( 3, ( #9417, #8075, #5967, #3604 ),
 .UNSPECIFIED., .F., .F. ) 
 B_SPLINE_CURVE_WITH_KNOTS ( ( 4, 4 ),
 ( 3.003391341741618259, 3.049711720517707114 ),
 .UNSPECIFIED. ) 
 CURVE ( )  GEOMETRIC_REPRESENTATION_ITEM ( )  RATIONAL_B_SPLINE_CURVE ( ( 1.000000000000000000, 0.9998212098678860293, 0.9998212098678860293, 1.000000000000000000 ) ) 
 REPRESENTATION_ITEM ( '' )  );
#3584=DIRECTION ( 'NONE',  ( 0.000000000000000000, 0.000000000000000000, 1.000000000000000000 ) ) ;
#3588=EDGE_LOOP ( 'NONE', ( #5027, #8009, #4390, #2057, #2597, #7834 ) ) ;
#3590=CARTESIAN_POINT ( 'NONE',  ( 37.00000000000000000, -8.017766952966340455, -116.9822330470336453 ) ) ;
#3593=AXIS2_PLACEMENT_3D ( 'NONE', #9226, #4098, #3374 ) ;
#3595=CARTESIAN_POINT ( 'NONE',  ( 53.29490495164537833, -30.00000000000000000, -100.0000000000000000 ) ) ;
#3596=ORIENTED_EDGE ( 'NONE', *, *, #19, .F. ) ;
#3597=ORIENTED_EDGE ( 'NONE', *, *, #6263, .F. ) ;
#3598=ORIENTED_EDGE ( 'NONE', *, *, #5962, .T. ) ;
#3603=EDGE_CURVE ( 'NONE', #8277, #3283, #8923, .T. ) ;
#3604=CARTESIAN_POINT ( 'NONE',  ( 51.96152422706632734, 30.00000000000000000, -80.85015119857381194 ) ) ;
#3606=CARTESIAN_POINT ( 'NONE',  ( -27.00000000000000000, -43.00000000000000000, 11.99999999999999645 ) ) ;
#3607=AXIS2_PLACEMENT_3D ( 'NONE', #6238, #2449, #1671 ) ;
#3608=EDGE_CURVE ( 'NONE', #8284, #8127, #5952, .T. ) ;
#3609=CARTESIAN_POINT ( 'NONE',  ( -26.21170834203224231, 53.97171801779369105, -2.612255525622730001 ) ) ;
#3618=LINE ( 'NONE', #5064, #3539 ) ;
#3620=AXIS2_PLACEMENT_3D ( 'NONE', #2144, #4262, #4929 ) ;
#3622=VERTEX_POINT ( 'NONE', #4609 ) ;
#3623=ORIENTED_EDGE ( 'NONE', *, *, #4754, .F. ) ;
#3629=DIRECTION ( 'NONE',  ( -0.000000000000000000, -0.000000000000000000, -1.000000000000000000 ) ) ;
#3633=EDGE_CURVE ( 'NONE', #2195, #4271, #2299, .T. ) ;
#3636=DIRECTION ( 'NONE',  ( 1.000000000000000000, -0.000000000000000000, -0.000000000000000000 ) ) ;
#3640=CARTESIAN_POINT ( 'NONE',  ( -26.21170834203230982, -53.97171801779368394, -2.612255525622733554 ) ) ;
#3646=( BOUNDED_CURVE ( )  B_SPLINE_CURVE ( 3, ( #314, #2525, #8286, #6762 ),
 .UNSPECIFIED., .F., .T. ) 
 B_SPLINE_CURVE_WITH_KNOTS ( ( 4, 4 ),
 ( 3.003391341741614262, 3.049711720517703117 ),
 .UNSPECIFIED. ) 
 CURVE ( )  GEOMETRIC_REPRESENTATION_ITEM ( )  RATIONAL_B_SPLINE_CURVE ( ( 1.000000000000000000, 0.9998212098678860293, 0.9998212098678860293, 1.000000000000000000 ) ) 
 REPRESENTATION_ITEM ( '' )  );
#3650=ORIENTED_EDGE ( 'NONE', *, *, #4300, .T. ) ;
#3653=EDGE_CURVE ( 'NONE', #8127, #5995, #147, .T. ) ;
#3655=ORIENTED_EDGE ( 'NONE', *, *, #8431, .F. ) ;
#3657=EDGE_CURVE ( 'NONE', #1974, #458, #9017, .T. ) ;
#3658=DIRECTION ( 'NONE',  ( -1.000000000000000000, 0.000000000000000000, 0.000000000000000000 ) ) ;
#3663=CARTESIAN_POINT ( 'NONE',  ( 53.29490495164537833, 15.90990257669733943, -54.09009742330271564 ) ) ;
#3667=DIRECTION ( 'NONE',  ( -1.000000000000000000, 0.000000000000000000, 0.000000000000000000 ) ) ;
#3668=ORIENTED_EDGE ( 'NONE', *, *, #5611, .T. ) ;
#3675=EDGE_LOOP ( 'NONE', ( #2963, #6802 ) ) ;
#3677=ORIENTED_EDGE ( 'NONE', *, *, #6373, .F. ) ;
#3678=DIRECTION ( 'NONE',  ( -0.000000000000000000, -0.000000000000000000, 1.000000000000000000 ) ) ;
#3679=CARTESIAN_POINT ( 'NONE',  ( -34.25000000000000000, -43.00000000000000000, 11.99999999999999645 ) ) ;
#3689=PLANE ( 'NONE',  #7166 ) ;
#3690=VECTOR ( 'NONE', #8910, 1000.000000000000000 ) ;
#3693=ORIENTED_EDGE ( 'NONE', *, *, #3975, .F. ) ;
#3694=ORIENTED_EDGE ( 'NONE', *, *, #5679, .F. ) ;
#3699=( BOUNDED_CURVE ( )  B_SPLINE_CURVE ( 3, ( #1425, #8874, #5998, #3640 ),
 .UNSPECIFIED., .F., .T. ) 
 B_SPLINE_CURVE_WITH_KNOTS ( ( 4, 4 ),
 ( 1.570796326794896558, 3.069868295139984049 ),
 .UNSPECIFIED. ) 
 CURVE ( )  GEOMETRIC_REPRESENTATION_ITEM ( )  RATIONAL_B_SPLINE_CURVE ( ( 1.000000000000000000, 0.8213367208436757050, 0.8213367208436757050, 1.000000000000000000 ) ) 
 REPRESENTATION_ITEM ( '' )  );
#3704=CARTESIAN_POINT ( 'NONE',  ( -40.00000000000000000, 0.000000000000000000, -13.00000000000000533 ) ) ;
#3706=ADVANCED_FACE ( 'NONE', ( #7579 ), #997, .F. ) ;
#3707=CARTESIAN_POINT ( 'NONE',  ( 60.00000000000000000, -30.00000000000000355, -82.50000000000001421 ) ) ;
#3710=CARTESIAN_POINT ( 'NONE',  ( 16.00000000000000000, 43.00000000000000000, -7.366666666666667140 ) ) ;
#3713=ORIENTED_EDGE ( 'NONE', *, *, #8303, .F. ) ;
#3714=CIRCLE ( 'NONE', #2796, 3.000000000000002665 ) ;
#3715=DIRECTION ( 'NONE',  ( 0.000000000000000000, 0.000000000000000000, -1.000000000000000000 ) ) ;
#3717=FACE_OUTER_BOUND ( 'NONE', #3566, .T. ) ;
#3718=CARTESIAN_POINT ( 'NONE',  ( -62.09859669818813899, -30.00000000000000000, -66.51416582715449977 ) ) ;
#3724=DIRECTION ( 'NONE',  ( 0.000000000000000000, 0.000000000000000000, -1.000000000000000000 ) ) ;
#3725=LINE ( 'NONE', #8046, #587 ) ;
#3727=CARTESIAN_POINT ( 'NONE',  ( -27.00000000000000000, 43.00000000000000000, 25.00000000000000000 ) ) ;
#3728=DIRECTION ( 'NONE',  ( 0.000000000000000000, 0.000000000000000000, -1.000000000000000000 ) ) ;
#3734=ORIENTED_EDGE ( 'NONE', *, *, #2823, .F. ) ;
#3737=ORIENTED_EDGE ( 'NONE', *, *, #9345, .T. ) ;
#3740=UNCERTAINTY_MEASURE_WITH_UNIT (LENGTH_MEASURE( 1.000000000000000082E-05 ), #8042, 'distance_accuracy_value', 'NONE');
#3741=LINE ( 'NONE', #854, #3475 ) ;
#3748=CARTESIAN_POINT ( 'NONE',  ( -34.25000000000000000, 43.00000000000000000, 11.99999999999999645 ) ) ;
#3753=DIRECTION ( 'NONE',  ( -0.7071067811865441310, -0.5000000000000026645, 0.5000000000000023315 ) ) ;
#3757=VECTOR ( 'NONE', #6260, 1000.000000000000000 ) ;
#3763=CYLINDRICAL_SURFACE ( 'NONE', #2646, 3.000000000000002665 ) ;
#3764=ORIENTED_EDGE ( 'NONE', *, *, #7665, .F. ) ;
#3765=VERTEX_POINT ( 'NONE', #3256 ) ;
#3768=EDGE_LOOP ( 'NONE', ( #1025, #96, #9087, #3596 ) ) ;
#3769=CARTESIAN_POINT ( 'NONE',  ( -28.61406079152386894, 10.49089634068029575, -86.61406079152385473 ) ) ;
#3770=DIRECTION ( 'NONE',  ( 0.000000000000000000, 0.000000000000000000, -1.000000000000000000 ) ) ;
#3771=ADVANCED_FACE ( 'NONE', ( #6916 ), #4703, .F. ) ;
#3772=CARTESIAN_POINT ( 'NONE',  ( 57.72192878071319910, 19.00148731544556568, -33.94573509506513176 ) ) ;
#3774=CIRCLE ( 'NONE', #395, 11.00000000000000711 ) ;
#3783=ORIENTED_EDGE ( 'NONE', *, *, #6373, .T. ) ;
#3785=CARTESIAN_POINT ( 'NONE',  ( -41.99999999999999289, -30.00000000000000000, -100.0000000000000000 ) ) ;
#3796=AXIS2_PLACEMENT_3D ( 'NONE', #7819, #5473, #8398 ) ;
#3806=CIRCLE ( 'NONE', #7032, 3.000000000000002665 ) ;
#3809=EDGE_CURVE ( 'NONE', #4380, #1809, #8193, .T. ) ;
#3818=EDGE_LOOP ( 'NONE', ( #8375, #7416, #5415, #8477, #3694 ) ) ;
#3820=CARTESIAN_POINT ( 'NONE',  ( 60.00000000000000000, -15.90990257669733943, -51.09009742330271564 ) ) ;
#3824=CARTESIAN_POINT ( 'NONE',  ( 51.96152422706632734, -30.00000000000000000, -134.0000000000000284 ) ) ;
#3825=PLANE ( 'NONE',  #3593 ) ;
#3827=ORIENTED_EDGE ( 'NONE', *, *, #633, .F. ) ;
#3831=DIRECTION ( 'NONE',  ( 0.000000000000000000, -1.000000000000000000, 0.000000000000000000 ) ) ;
#3832=LINE ( 'NONE', #4502, #1665 ) ;
#3834=EDGE_CURVE ( 'NONE', #6367, #1132, #8450, .T. ) ;
#3835=ORIENTED_EDGE ( 'NONE', *, *, #5611, .F. ) ;
#3837=VECTOR ( 'NONE', #9383, 999.9999999999998863 ) ;
#3848=CARTESIAN_POINT ( 'NONE',  ( -53.29490495164537833, 18.67545040036925386, -90.28901569369799063 ) ) ;
#3849=DIRECTION ( 'NONE',  ( 0.000000000000000000, 0.000000000000000000, -1.000000000000000000 ) ) ;
#3853=AXIS2_PLACEMENT_3D ( 'NONE', #7851, #7895, #8716 ) ;
#3857=PLANE ( 'NONE',  #4037 ) ;
#3859=DIRECTION ( 'NONE',  ( 0.000000000000000000, -0.3976074376343005090, -0.9175556253099241832 ) ) ;
#3861=VERTEX_POINT ( 'NONE', #7137 ) ;
#3863=ORIENTED_EDGE ( 'NONE', *, *, #2717, .F. ) ;
#3864=VERTEX_POINT ( 'NONE', #559 ) ;
#3876=VERTEX_POINT ( 'NONE', #3438 ) ;
#3877=EDGE_LOOP ( 'NONE', ( #4438, #1808 ) ) ;
#3879=ORIENTED_EDGE ( 'NONE', *, *, #4233, .T. ) ;
#3880=FACE_BOUND ( 'NONE', #9365, .T. ) ;
#3883=DIRECTION ( 'NONE',  ( 0.000000000000000000, 0.000000000000000000, -1.000000000000000000 ) ) ;
#3888=VERTEX_POINT ( 'NONE', #1323 ) ;
#3892=DIRECTION ( 'NONE',  ( 0.000000000000000000, -0.000000000000000000, 1.000000000000000000 ) ) ;
#3897=EDGE_CURVE ( 'NONE', #2826, #6270, #2145, .T. ) ;
#3898=CARTESIAN_POINT ( 'NONE',  ( 51.96152422706632734, 30.00000000000000000, -80.85015119857381194 ) ) ;
#3899=ORIENTED_EDGE ( 'NONE', *, *, #728, .T. ) ;
#3900=CIRCLE ( 'NONE', #4061, 7.250000000000002665 ) ;
#3905=CARTESIAN_POINT ( 'NONE',  ( 19.74999999999999645, -43.00000000000000000, 25.00000000000000000 ) ) ;
#3906=DIRECTION ( 'NONE',  ( 0.000000000000000000, 0.000000000000000000, 1.000000000000000000 ) ) ;
#3914=CARTESIAN_POINT ( 'NONE',  ( 57.72192878071321331, -19.00148731544555147, -33.94573509506509623 ) ) ;
#3917=CARTESIAN_POINT ( 'NONE',  ( 53.29490495164537833, -15.90990257669733943, -85.90990257669729147 ) ) ;
#3921=CARTESIAN_POINT ( 'NONE',  ( -19.74999999999999645, -43.00000000000000000, 25.00000000000000000 ) ) ;
#3923=EDGE_LOOP ( 'NONE', ( #4172, #7155 ) ) ;
#3925=DIRECTION ( 'NONE',  ( -1.000000000000000000, 0.000000000000000000, 0.000000000000000000 ) ) ;
#3926=VERTEX_POINT ( 'NONE', #8005 ) ;
#3932=CARTESIAN_POINT ( 'NONE',  ( -26.21170834203230982, -53.97171801779368394, -2.612255525622733554 ) ) ;
#3933=CARTESIAN_POINT ( 'NONE',  ( 0.000000000000000000, 0.000000000000000000, 25.00000000000000000 ) ) ;
#3937=ORIENTED_EDGE ( 'NONE', *, *, #8431, .T. ) ;
#3939=AXIS2_PLACEMENT_3D ( 'NONE', #5100, #2985, #9424 ) ;
#3945=PRODUCT_DEFINITION ( 'UNKNOWN', '', #3450, #6065 ) ;
#3950=EDGE_CURVE ( 'NONE', #6722, #4533, #7528, .T. ) ;
#3956=DIRECTION ( 'NONE',  ( 0.000000000000000000, -0.000000000000000000, 1.000000000000000000 ) ) ;
#3960=AXIS2_PLACEMENT_3D ( 'NONE', #47, #89, #2242 ) ;
#3969=CARTESIAN_POINT ( 'NONE',  ( -19.74999999999999645, -43.00000000000000000, -25.00000000000000000 ) ) ;
#3972=ADVANCED_FACE ( 'NONE', ( #4310, #2093, #7966, #7233, #6805, #3004 ), #2956, .T. ) ;
#3974=CIRCLE ( 'NONE', #3199, 11.00000000000000000 ) ;
#3975=EDGE_CURVE ( 'NONE', #7674, #1938, #4154, .T. ) ;
#3976=CARTESIAN_POINT ( 'NONE',  ( -37.22467645238198486, 47.05659850664388699, -0.5000000000000038858 ) ) ;
#3979=ORIENTED_EDGE ( 'NONE', *, *, #37, .T. ) ;
#3986=DIRECTION ( 'NONE',  ( 0.000000000000000000, 0.000000000000000000, -1.000000000000000000 ) ) ;
#3989=DIRECTION ( 'NONE',  ( -0.000000000000000000, -0.000000000000000000, -1.000000000000000000 ) ) ;
#3990=DIRECTION ( 'NONE',  ( -1.000000000000000000, 0.000000000000000000, 0.000000000000000000 ) ) ;
#3991=ORIENTED_EDGE ( 'NONE', *, *, #9118, .T. ) ;
#3995=CARTESIAN_POINT ( 'NONE',  ( 60.00000000000000000, -1.836970198721028011E-15, -85.00000000000000000 ) ) ;
#3999=FACE_OUTER_BOUND ( 'NONE', #741, .T. ) ;
#4000=ORIENTED_EDGE ( 'NONE', *, *, #5717, .T. ) ;
#4001=LINE ( 'NONE', #345, #8850 ) ;
#4003=CARTESIAN_POINT ( 'NONE',  ( 37.22467645238198486, -47.05659850664387989, 11.99999999999999645 ) ) ;
#4004=LINE ( 'NONE', #5448, #6105 ) ;
#4007=CARTESIAN_POINT ( 'NONE',  ( 37.22467645238197775, -47.05659850664388699, -5.608807313787648852 ) ) ;
#4011=EDGE_CURVE ( 'NONE', #7415, #975, #7374, .T. ) ;
#4012=ADVANCED_FACE ( 'NONE', ( #4398 ), #8817, .F. ) ;
#4016=ORIENTED_EDGE ( 'NONE', *, *, #830, .T. ) ;
#4018=CYLINDRICAL_SURFACE ( 'NONE', #3171, 60.00000000000000000 ) ;
#4024=LINE ( 'NONE', #9103, #4528 ) ;
#4029=ORIENTED_EDGE ( 'NONE', *, *, #2923, .F. ) ;
#4030=CIRCLE ( 'NONE', #8617, 11.00000000000000000 ) ;
#4033=PLANE ( 'NONE',  #8801 ) ;
#4034=CARTESIAN_POINT ( 'NONE',  ( 53.29490495164537833, 11.46446609406721961, -97.50000000000002842 ) ) ;
#4036=ORIENTED_EDGE ( 'NONE', *, *, #4886, .T. ) ;
#4037=AXIS2_PLACEMENT_3D ( 'NONE', #4725, #1649, #5356 ) ;
#4039=CARTESIAN_POINT ( 'NONE',  ( -27.00000000000000000, -43.00000000000000000, 11.99999999999999645 ) ) ;
#4045=ORIENTED_EDGE ( 'NONE', *, *, #7665, .T. ) ;
#4046=DIRECTION ( 'NONE',  ( -0.000000000000000000, -0.000000000000000000, 1.000000000000000000 ) ) ;
#4051=EDGE_CURVE ( 'NONE', #4256, #5417, #789, .T. ) ;
#4052=FACE_OUTER_BOUND ( 'NONE', #681, .T. ) ;
#4053=LINE ( 'NONE', #6278, #4324 ) ;
#4054=VECTOR ( 'NONE', #802, 999.9999999999998863 ) ;
#4056=ORIENTED_EDGE ( 'NONE', *, *, #6004, .T. ) ;
#4058=ORIENTED_EDGE ( 'NONE', *, *, #4113, .F. ) ;
#4061=AXIS2_PLACEMENT_3D ( 'NONE', #7485, #3303, #3213 ) ;
#4065=EDGE_LOOP ( 'NONE', ( #7025, #8723, #7925, #6823, #2948, #7979 ) ) ;
#4068=PLANE ( 'NONE',  #2092 ) ;
#4079=VERTEX_POINT ( 'NONE', #4452 ) ;
#4086=CYLINDRICAL_SURFACE ( 'NONE', #8412, 3.000000000000002665 ) ;
#4095=DIRECTION ( 'NONE',  ( -1.000000000000000000, 0.000000000000000000, 0.000000000000000000 ) ) ;
#4096=DIRECTION ( 'NONE',  ( -0.000000000000000000, -0.000000000000000000, -1.000000000000000000 ) ) ;
#4098=DIRECTION ( 'NONE',  ( 0.000000000000000000, 0.3976074376343005090, -0.9175556253099241832 ) ) ;
#4113=EDGE_CURVE ( 'NONE', #3384, #6270, #896, .T. ) ;
#4118=CARTESIAN_POINT ( 'NONE',  ( 26.21170834203226718, -53.97171801779368394, -2.612255525622730001 ) ) ;
#4120=VECTOR ( 'NONE', #4928, 1000.000000000000000 ) ;
#4124=EDGE_CURVE ( 'NONE', #458, #1534, #749, .T. ) ;
#4138=ORIENTED_EDGE ( 'NONE', *, *, #4994, .T. ) ;
#4139=EDGE_CURVE ( 'NONE', #4458, #7922, #8599, .T. ) ;
#4144=CARTESIAN_POINT ( 'NONE',  ( -27.00000000000000000, 43.00000000000000000, 11.99999999999999645 ) ) ;
#4145=DIRECTION ( 'NONE',  ( 1.000000000000000000, 0.000000000000000000, 0.000000000000000000 ) ) ;
#4147=FACE_OUTER_BOUND ( 'NONE', #5628, .T. ) ;
#4154=CIRCLE ( 'NONE', #3233, 15.00000000000000000 ) ;
#4155=CARTESIAN_POINT ( 'NONE',  ( 38.00000000000000000, 44.39318849903271769, -6.762951650419155136 ) ) ;
#4160=CARTESIAN_POINT ( 'NONE',  ( -15.99999999999999289, 20.99999999999999289, -16.89999999999999858 ) ) ;
#4161=VECTOR ( 'NONE', #6558, 1000.000000000000227 ) ;
#4164=DIRECTION ( 'NONE',  ( -0.000000000000000000, -0.000000000000000000, 1.000000000000000000 ) ) ;
#4165=CARTESIAN_POINT ( 'NONE',  ( 27.00000000000000000, -43.00000000000000000, 25.00000000000000000 ) ) ;
#4172=ORIENTED_EDGE ( 'NONE', *, *, #2719, .F. ) ;
#4185=CARTESIAN_POINT ( 'NONE',  ( -15.99999999999999645, -43.00000000000000000, -7.366666666666667140 ) ) ;
#4187=CARTESIAN_POINT ( 'NONE',  ( -53.29490495164537833, -15.90990257669733943, -85.90990257669729147 ) ) ;
#4195=AXIS2_PLACEMENT_3D ( 'NONE', #8221, #8719, #5066 ) ;
#4198=CARTESIAN_POINT ( 'NONE',  ( -53.29490495164537833, 15.90990257669733943, -54.09009742330271564 ) ) ;
#4200=ORIENTED_EDGE ( 'NONE', *, *, #251, .F. ) ;
#4202=LINE ( 'NONE', #7956, #1945 ) ;
#4218=DIRECTION ( 'NONE',  ( -1.000000000000000000, 0.000000000000000000, -0.000000000000000000 ) ) ;
#4220=CARTESIAN_POINT ( 'NONE',  ( 50.79490495164537833, 12.50000000000000000, -100.0000000000000000 ) ) ;
#4223=VERTEX_POINT ( 'NONE', #3244 ) ;
#4225=EDGE_CURVE ( 'NONE', #5660, #3926, #1706, .T. ) ;
#4228=CARTESIAN_POINT ( 'NONE',  ( 0.000000000000000000, 0.000000000000000000, 23.99999999999998579 ) ) ;
#4232=EDGE_CURVE ( 'NONE', #3144, #2690, #7715, .T. ) ;
#4233=EDGE_CURVE ( 'NONE', #8754, #3144, #7670, .T. ) ;
#4234=CARTESIAN_POINT ( 'NONE',  ( 34.25000000000000000, -43.00000000000000000, 25.00000000000000000 ) ) ;
#4241=CARTESIAN_POINT ( 'NONE',  ( -50.79490495164537833, -30.00000000000000000, -100.0000000000000000 ) ) ;
#4242=CARTESIAN_POINT ( 'NONE',  ( 38.00000000000000000, 43.00000000000000000, -7.366666666666667140 ) ) ;
#4249=DIRECTION ( 'NONE',  ( -1.000000000000000000, 0.000000000000000000, 0.000000000000000000 ) ) ;
#4252=EDGE_CURVE ( 'NONE', #955, #2481, #2579, .T. ) ;
#4253=ORIENTED_EDGE ( 'NONE', *, *, #4715, .T. ) ;
#4254=LINE ( 'NONE', #7766, #3321 ) ;
#4255=AXIS2_PLACEMENT_3D ( 'NONE', #795, #8158, #7428 ) ;
#4256=VERTEX_POINT ( 'NONE', #6187 ) ;
#4257=EDGE_CURVE ( 'NONE', #5515, #6613, #2927, .T. ) ;
#4262=DIRECTION ( 'NONE',  ( -0.000000000000000000, -0.000000000000000000, 1.000000000000000000 ) ) ;
#4267=( BOUNDED_CURVE ( )  B_SPLINE_CURVE ( 3, ( #8015, #6532, #2969, #6584 ),
 .UNSPECIFIED., .F., .T. ) 
 B_SPLINE_CURVE_WITH_KNOTS ( ( 4, 4 ),
 ( 1.570796326794896558, 1.948494305174372832 ),
 .UNSPECIFIED. ) 
 CURVE ( )  GEOMETRIC_REPRESENTATION_ITEM ( )  RATIONAL_B_SPLINE_CURVE ( ( 1.000000000000000000, 0.9881473088045071851, 0.9881473088045071851, 1.000000000000000000 ) ) 
 REPRESENTATION_ITEM ( '' )  );
#4268=CARTESIAN_POINT ( 'NONE',  ( -72.75414293302374347, 30.00000000000000000, -51.44494782735612404 ) ) ;
#4271=VERTEX_POINT ( 'NONE', #8384 ) ;
#4286=CARTESIAN_POINT ( 'NONE',  ( 37.00000000000000711, -30.00000000000000000, -13.00000000000000000 ) ) ;
#4296=CARTESIAN_POINT ( 'NONE',  ( 0.000000000000000000, 0.000000000000000000, 11.99999999999999645 ) ) ;
#4299=EDGE_CURVE ( 'NONE', #8200, #2677, #6468, .T. ) ;
#4300=EDGE_CURVE ( 'NONE', #9426, #3888, #3618, .T. ) ;
#4303=EDGE_LOOP ( 'NONE', ( #1345, #7559, #8807, #6646 ) ) ;
#4310=FACE_BOUND ( 'NONE', #188, .T. ) ;
#4315=ORIENTED_EDGE ( 'NONE', *, *, #8741, .T. ) ;
#4316=VERTEX_POINT ( 'NONE', #6509 ) ;
#4321=( BOUNDED_CURVE ( )  B_SPLINE_CURVE ( 3, ( #6354, #2701, #7207, #4185 ),
 .UNSPECIFIED., .F., .T. ) 
 B_SPLINE_CURVE_WITH_KNOTS ( ( 4, 4 ),
 ( 4.712388980384689674, 7.853981633974482790 ),
 .UNSPECIFIED. ) 
 CURVE ( )  GEOMETRIC_REPRESENTATION_ITEM ( )  RATIONAL_B_SPLINE_CURVE ( ( 1.000000000000000000, 0.3333333333333333703, 0.3333333333333333703, 1.000000000000000000 ) ) 
 REPRESENTATION_ITEM ( '' )  );
#4324=VECTOR ( 'NONE', #6219, 1000.000000000000000 ) ;
#4325=ORIENTED_EDGE ( 'NONE', *, *, #3653, .F. ) ;
#4329=CYLINDRICAL_SURFACE ( 'NONE', #3312, 3.000000000000002665 ) ;
#4338=CYLINDRICAL_SURFACE ( 'NONE', #2715, 11.00000000000000000 ) ;
#4347=VECTOR ( 'NONE', #4249, 1000.000000000000000 ) ;
#4350=EDGE_LOOP ( 'NONE', ( #9228, #3573 ) ) ;
#4352=DIRECTION ( 'NONE',  ( -1.000000000000000000, 0.000000000000000000, 0.000000000000000000 ) ) ;
#4354=CARTESIAN_POINT ( 'NONE',  ( -27.00000000000000000, -43.00000000000000000, 11.99999999999999645 ) ) ;
#4357=EDGE_CURVE ( 'NONE', #5609, #5683, #1389, .T. ) ;
#4363=VERTEX_POINT ( 'NONE', #4965 ) ;
#4365=CARTESIAN_POINT ( 'NONE',  ( -50.79490495164537833, 29.99999999999999645, -82.50000000000000000 ) ) ;
#4374=CARTESIAN_POINT ( 'NONE',  ( 60.00000000000000000, -15.90990257669733943, -88.90990257669730568 ) ) ;
#4375=CARTESIAN_POINT ( 'NONE',  ( 53.29490495164537833, 27.56180520566615044, -81.40266088840108694 ) ) ;
#4380=VERTEX_POINT ( 'NONE', #2081 ) ;
#4381=CARTESIAN_POINT ( 'NONE',  ( 16.00000000000000000, 49.08300322764475254, -4.730698601353941157 ) ) ;
#4390=ORIENTED_EDGE ( 'NONE', *, *, #8637, .T. ) ;
#4395=VECTOR ( 'NONE', #2126, 999.9999999999998863 ) ;
#4396=DIRECTION ( 'NONE',  ( 0.000000000000000000, 0.7071067811865473507, 0.7071067811865477948 ) ) ;
#4397=VECTOR ( 'NONE', #8865, 1000.000000000000000 ) ;
#4398=FACE_OUTER_BOUND ( 'NONE', #7633, .T. ) ;
#4400=EDGE_CURVE ( 'NONE', #3765, #8325, #2362, .T. ) ;
#4409=VECTOR ( 'NONE', #7739, 1000.000000000000000 ) ;
#4411=DIRECTION ( 'NONE',  ( -0.000000000000000000, -0.000000000000000000, 1.000000000000000000 ) ) ;
#4412=AXIS2_PLACEMENT_3D ( 'NONE', #3848, #6063, #6013 ) ;
#4414=EDGE_CURVE ( 'NONE', #4692, #4881, #7125, .T. ) ;
#4417=EDGE_CURVE ( 'NONE', #3211, #7343, #473, .T. ) ;
#4418=EDGE_CURVE ( 'NONE', #6367, #1975, #1979, .T. ) ;
#4420=CARTESIAN_POINT ( 'NONE',  ( 9.364477336218625325, 62.15368297487813010, 0.9332626224471926024 ) ) ;
#4426=DIRECTION ( 'NONE',  ( 0.000000000000000000, 0.000000000000000000, 1.000000000000000000 ) ) ;
#4427=VECTOR ( 'NONE', #5114, 1000.000000000000000 ) ;
#4434=EDGE_CURVE ( 'NONE', #5694, #7596, #7219, .T. ) ;
#4438=ORIENTED_EDGE ( 'NONE', *, *, #7615, .T. ) ;
#4445=ORIENTED_EDGE ( 'NONE', *, *, #8643, .T. ) ;
#4452=CARTESIAN_POINT ( 'NONE',  ( -51.96152422706631313, 30.00000000000000711, -12.99999999999999289 ) ) ;
#4458=VERTEX_POINT ( 'NONE', #5834 ) ;
#4459=CARTESIAN_POINT ( 'NONE',  ( 50.79490495164537833, -30.00000000000000000, -100.0000000000000000 ) ) ;
#4461=EDGE_CURVE ( 'NONE', #1938, #7674, #8575, .T. ) ;
#4463=AXIS2_PLACEMENT_3D ( 'NONE', #3917, #6991, #4784 ) ;
#4465=CARTESIAN_POINT ( 'NONE',  ( -26.21170834203224231, 53.97171801779369105, -2.612255525622730001 ) ) ;
#4474=DIRECTION ( 'NONE',  ( -1.000000000000000000, 0.000000000000000000, -0.000000000000000000 ) ) ;
#4478=VERTEX_POINT ( 'NONE', #6227 ) ;
#4479=VECTOR ( 'NONE', #4764, 1000.000000000000000 ) ;
#4483=FACE_OUTER_BOUND ( 'NONE', #2794, .T. ) ;
#4490=DIRECTION ( 'NONE',  ( 0.000000000000000000, 0.000000000000000000, -1.000000000000000000 ) ) ;
#4491=CARTESIAN_POINT ( 'NONE',  ( -37.00000000000000711, -15.90990257669733943, -54.09009742330271564 ) ) ;
#4493=CARTESIAN_POINT ( 'NONE',  ( 59.00000000000000000, 7.225416114969383207E-15, 25.00000000000000000 ) ) ;
#4495=AXIS2_PLACEMENT_3D ( 'NONE', #5488, #8273, #8418 ) ;
#4502=CARTESIAN_POINT ( 'NONE',  ( 60.00000000000000000, -12.50000000000000000, -100.0000000000000000 ) ) ;
#4506=FACE_BOUND ( 'NONE', #1092, .T. ) ;
#4512=AXIS2_PLACEMENT_3D ( 'NONE', #1324, #5574, #1966 ) ;
#4513=LINE ( 'NONE', #5344, #1162 ) ;
#4515=CIRCLE ( 'NONE', #6364, 15.00000000000000000 ) ;
#4517=DIRECTION ( 'NONE',  ( -0.000000000000000000, 0.000000000000000000, 1.000000000000000000 ) ) ;
#4519=CARTESIAN_POINT ( 'NONE',  ( -37.00000000000000000, -13.96446609406728712, -95.00000000000000000 ) ) ;
#4520=DIRECTION ( 'NONE',  ( 0.000000000000000000, 0.000000000000000000, 1.000000000000000000 ) ) ;
#4521=CARTESIAN_POINT ( 'NONE',  ( -15.99999999999999645, -43.00000000000000000, -7.366666666666667140 ) ) ;
#4522=VERTEX_POINT ( 'NONE', #1552 ) ;
#4523=DIRECTION ( 'NONE',  ( -1.000000000000000000, -0.000000000000000000, -0.000000000000000000 ) ) ;
#4524=VECTOR ( 'NONE', #6785, 999.9999999999998863 ) ;
#4525=ORIENTED_EDGE ( 'NONE', *, *, #1009, .T. ) ;
#4528=VECTOR ( 'NONE', #8296, 1000.000000000000000 ) ;
#4532=ADVANCED_FACE ( 'NONE', ( #3717 ), #7363, .T. ) ;
#4533=VERTEX_POINT ( 'NONE', #8851 ) ;
#4539=DIRECTION ( 'NONE',  ( 1.000000000000000000, 0.000000000000000000, 0.000000000000000000 ) ) ;
#4540=VERTEX_POINT ( 'NONE', #116 ) ;
#4555=AXIS2_PLACEMENT_3D ( 'NONE', #7419, #1463, #788 ) ;
#4558=ORIENTED_EDGE ( 'NONE', *, *, #6547, .F. ) ;
#4560=AXIS2_PLACEMENT_3D ( 'NONE', #7700, #304, #971 ) ;
#4561=DIRECTION ( 'NONE',  ( 0.000000000000000000, 0.000000000000000000, 1.000000000000000000 ) ) ;
#4568=AXIS2_PLACEMENT_3D ( 'NONE', #337, #5391, #1006 ) ;
#4569=CARTESIAN_POINT ( 'NONE',  ( 27.00000000000000000, 43.00000000000000000, 11.99999999999999645 ) ) ;
#4570=CARTESIAN_POINT ( 'NONE',  ( -37.22467645238203460, -47.05659850664382304, -5.608807313787673721 ) ) ;
#4574=CARTESIAN_POINT ( 'NONE',  ( 37.00000000000000000, -30.00000000000000000, -78.96446609406730488 ) ) ;
#4577=( BOUNDED_CURVE ( )  B_SPLINE_CURVE ( 3, ( #8972, #1089, #1818, #9159 ),
 .UNSPECIFIED., .F., .T. ) 
 B_SPLINE_CURVE_WITH_KNOTS ( ( 4, 4 ),
 ( 3.233473586661880450, 3.279793965437969749 ),
 .UNSPECIFIED. ) 
 CURVE ( )  GEOMETRIC_REPRESENTATION_ITEM ( )  RATIONAL_B_SPLINE_CURVE ( ( 1.000000000000000000, 0.9998212098678860293, 0.9998212098678860293, 1.000000000000000000 ) ) 
 REPRESENTATION_ITEM ( '' )  );
#4580=AXIS2_PLACEMENT_3D ( 'NONE', #7624, #6241, #2637 ) ;
#4587=VECTOR ( 'NONE', #2757, 999.9999999999998863 ) ;
#4589=EDGE_LOOP ( 'NONE', ( #6282, #5691, #3330 ) ) ;
#4590=ORIENTED_EDGE ( 'NONE', *, *, #2624, .T. ) ;
#4593=CARTESIAN_POINT ( 'NONE',  ( -39.50000000000000711, 29.99999999999999645, -82.50000000000000000 ) ) ;
#4595=DIRECTION ( 'NONE',  ( -1.000000000000000000, 0.000000000000000000, 0.000000000000000000 ) ) ;
#4596=EDGE_CURVE ( 'NONE', #5974, #3120, #973, .T. ) ;
#4609=CARTESIAN_POINT ( 'NONE',  ( -37.00000000000000000, -30.00000000000000000, -12.99999999999999822 ) ) ;
#4610=FACE_OUTER_BOUND ( 'NONE', #5138, .T. ) ;
#4616=CARTESIAN_POINT ( 'NONE',  ( 50.79490495164537833, -30.00000000000000355, -82.50000000000001421 ) ) ;
#4619=( NAMED_UNIT ( * ) SI_UNIT ( $, .STERADIAN. ) SOLID_ANGLE_UNIT ( ) );
#4623=VERTEX_POINT ( 'NONE', #7656 ) ;
#4627=DIRECTION ( 'NONE',  ( -1.000000000000000000, 0.000000000000000000, 0.000000000000000000 ) ) ;
#4632=DIRECTION ( 'NONE',  ( -1.000000000000000000, 0.000000000000000000, 0.000000000000000000 ) ) ;
#4635=ORIENTED_EDGE ( 'NONE', *, *, #6758, .T. ) ;
#4639=DIRECTION ( 'NONE',  ( 0.000000000000000000, 0.000000000000000000, 1.000000000000000000 ) ) ;
#4644=FACE_OUTER_BOUND ( 'NONE', #6876, .T. ) ;
#4652=ORIENTED_EDGE ( 'NONE', *, *, #894, .T. ) ;
#4655=DIRECTION ( 'NONE',  ( 0.000000000000000000, 0.7071067811865473507, 0.7071067811865477948 ) ) ;
#4656=ADVANCED_FACE ( 'NONE', ( #4052 ), #9183, .F. ) ;
#4658=ADVANCED_FACE ( 'NONE', ( #8373 ), #215, .T. ) ;
#4659=FACE_BOUND ( 'NONE', #3923, .T. ) ;
#4660=DIRECTION ( 'NONE',  ( 0.6785983445458481089, -0.2810846377148337183, 0.6785983445458404484 ) ) ;
#4661=EDGE_LOOP ( 'NONE', ( #8476, #5123 ) ) ;
#4667=CARTESIAN_POINT ( 'NONE',  ( 53.29490495164537833, 18.67545040036925386, -90.28901569369799063 ) ) ;
#4682=CARTESIAN_POINT ( 'NONE',  ( -39.50000000000000711, 29.99999999999999645, -82.50000000000000000 ) ) ;
#4683=EDGE_LOOP ( 'NONE', ( #3306, #2435, #481, #1210 ) ) ;
#4684=ORIENTED_EDGE ( 'NONE', *, *, #9101, .F. ) ;
#4686=ORIENTED_EDGE ( 'NONE', *, *, #5824, .F. ) ;
#4688=DIRECTION ( 'NONE',  ( 0.000000000000000000, -0.7071067811865473507, -0.7071067811865477948 ) ) ;
#4692=VERTEX_POINT ( 'NONE', #8806 ) ;
#4698=ORIENTED_EDGE ( 'NONE', *, *, #7654, .T. ) ;
#4703=CYLINDRICAL_SURFACE ( 'NONE', #3796, 7.250000000000002665 ) ;
#4707=ORIENTED_EDGE ( 'NONE', *, *, #4461, .T. ) ;
#4708=EDGE_LOOP ( 'NONE', ( #2971, #394 ) ) ;
#4711=PLANE ( 'NONE',  #4412 ) ;
#4714=EDGE_CURVE ( 'NONE', #1397, #8147, #305, .T. ) ;
#4715=EDGE_CURVE ( 'NONE', #8690, #3384, #2844, .T. ) ;
#4716=LINE ( 'NONE', #4667, #4524 ) ;
#4718=CARTESIAN_POINT ( 'NONE',  ( 60.00000000000000000, -3.673940397442057600E-15, -70.00000000000000000 ) ) ;
#4720=CARTESIAN_POINT ( 'NONE',  ( 53.29490495164537833, -27.56180520566615044, -41.61356529332876875 ) ) ;
#4721=VECTOR ( 'NONE', #7144, 1000.000000000000000 ) ;
#4722=ORIENTED_EDGE ( 'NONE', *, *, #3123, .T. ) ;
#4723=CARTESIAN_POINT ( 'NONE',  ( 60.00000000000000000, -1.836970198721028011E-15, -85.00000000000000000 ) ) ;
#4724=ORIENTED_EDGE ( 'NONE', *, *, #8544, .F. ) ;
#4725=CARTESIAN_POINT ( 'NONE',  ( 0.000000000000000000, 30.00000000000000000, 0.000000000000000000 ) ) ;
#4729=CIRCLE ( 'NONE', #1151, 60.00000000000000000 ) ;
#4732=EDGE_LOOP ( 'NONE', ( #1770, #74, #6159, #1074 ) ) ;
#4734=EDGE_LOOP ( 'NONE', ( #3295, #7708, #4590, #2483 ) ) ;
#4742=CARTESIAN_POINT ( 'NONE',  ( -48.15955140082795793, 36.58521010404107443, -10.14640895491552897 ) ) ;
#4746=DIRECTION ( 'NONE',  ( -0.4999999999999977240, 0.000000000000000000, 0.8660254037844399289 ) ) ;
#4747=AXIS2_PLACEMENT_3D ( 'NONE', #2438, #7562, #9000 ) ;
#4750=AXIS2_PLACEMENT_3D ( 'NONE', #8800, #2903, #738 ) ;
#4754=EDGE_CURVE ( 'NONE', #8277, #3453, #1070, .T. ) ;
#4755=FACE_BOUND ( 'NONE', #9446, .T. ) ;
#4759=ADVANCED_FACE ( 'NONE', ( #4860 ), #9224, .F. ) ;
#4764=DIRECTION ( 'NONE',  ( -0.000000000000000000, -0.000000000000000000, -1.000000000000000000 ) ) ;
#4769=VECTOR ( 'NONE', #5572, 1000.000000000000000 ) ;
#4773=CARTESIAN_POINT ( 'NONE',  ( 60.00000000000000000, 15.90990257669733943, -54.09009742330271564 ) ) ;
#4777=EDGE_CURVE ( 'NONE', #5110, #4995, #7652, .T. ) ;
#4781=VERTEX_POINT ( 'NONE', #3416 ) ;
#4782=CYLINDRICAL_SURFACE ( 'NONE', #1110, 7.250000000000002665 ) ;
#4784=DIRECTION ( 'NONE',  ( 0.000000000000000000, 0.000000000000000000, -1.000000000000000000 ) ) ;
#4789=PLANE ( 'NONE',  #2845 ) ;
#4796=CARTESIAN_POINT ( 'NONE',  ( 53.29490495164537833, -15.90990257669733943, -51.09009742330271564 ) ) ;
#4797=CARTESIAN_POINT ( 'NONE',  ( -37.22467645238198486, 47.05659850664388699, -5.608807313787648852 ) ) ;
#4804=DIRECTION ( 'NONE',  ( -0.000000000000000000, -0.000000000000000000, 1.000000000000000000 ) ) ;
#4806=CYLINDRICAL_SURFACE ( 'NONE', #4495, 7.250000000000002665 ) ;
#4808=VERTEX_POINT ( 'NONE', #5734 ) ;
#4810=CARTESIAN_POINT ( 'NONE',  ( -27.00000000000000000, -43.00000000000000000, 11.99999999999999645 ) ) ;
#4815=AXIS2_PLACEMENT_3D ( 'NONE', #666, #2879, #1577 ) ;
#4826=EDGE_CURVE ( 'NONE', #975, #2905, #1375, .T. ) ;
#4829=EDGE_CURVE ( 'NONE', #5974, #4623, #2301, .T. ) ;
#4842=EDGE_CURVE ( 'NONE', #5859, #438, #8424, .T. ) ;
#4843=ADVANCED_FACE ( 'NONE', ( #2027 ), #4952, .F. ) ;
#4844=DIRECTION ( 'NONE',  ( -0.000000000000000000, -0.000000000000000000, -1.000000000000000000 ) ) ;
#4853=CARTESIAN_POINT ( 'NONE',  ( 37.22467645238197775, -47.05659850664388699, -0.5000000000000038858 ) ) ;
#4859=CARTESIAN_POINT ( 'NONE',  ( -37.00000000000000000, -30.00000000000000000, -13.00000000000001066 ) ) ;
#4860=FACE_OUTER_BOUND ( 'NONE', #2179, .T. ) ;
#4861=CARTESIAN_POINT ( 'NONE',  ( -20.14434505884618076, 53.53579249963519970, -2.801156583491412722 ) ) ;
#4864=ORIENTED_EDGE ( 'NONE', *, *, #4994, .F. ) ;
#4865=ORIENTED_EDGE ( 'NONE', *, *, #5637, .F. ) ;
#4869=CIRCLE ( 'NONE', #9468, 3.000000000000002665 ) ;
#4871=VECTOR ( 'NONE', #2209, 1000.000000000000000 ) ;
#4878=ORIENTED_EDGE ( 'NONE', *, *, #805, .T. ) ;
#4881=VERTEX_POINT ( 'NONE', #9465 ) ;
#4883=CARTESIAN_POINT ( 'NONE',  ( 16.00000000000000000, -49.08300322764474544, -4.730698601353946486 ) ) ;
#4886=EDGE_CURVE ( 'NONE', #5944, #5804, #2598, .T. ) ;
#4887=DIRECTION ( 'NONE',  ( 0.000000000000000000, 0.000000000000000000, 1.000000000000000000 ) ) ;
#4889=CYLINDRICAL_SURFACE ( 'NONE', #4973, 3.000000000000002665 ) ;
#4894=AXIS2_PLACEMENT_3D ( 'NONE', #4296, #2673, #8665 ) ;
#4895=ORIENTED_EDGE ( 'NONE', *, *, #7439, .T. ) ;
#4899=DIRECTION ( 'NONE',  ( 0.000000000000000000, 0.7071067811865473507, 0.7071067811865477948 ) ) ;
#4905=CARTESIAN_POINT ( 'NONE',  ( 59.00000000000000000, 7.286648454926750781E-15, 25.00000000000000000 ) ) ;
#4906=FACE_OUTER_BOUND ( 'NONE', #64, .T. ) ;
#4911=CARTESIAN_POINT ( 'NONE',  ( 72.75414293302374347, 30.00000000000000000, -51.44494782735612404 ) ) ;
#4914=DIRECTION ( 'NONE',  ( -0.000000000000000000, -0.000000000000000000, 1.000000000000000000 ) ) ;
#4919=CARTESIAN_POINT ( 'NONE',  ( 37.00000000000000000, 15.90990257669733943, -57.09009742330271564 ) ) ;
#4922=PRODUCT_DEFINITION_SHAPE ( 'NONE', 'NONE',  #3945 ) ;
#4923=ORIENTED_EDGE ( 'NONE', *, *, #4051, .F. ) ;
#4927=LINE ( 'NONE', #5706, #295 ) ;
#4928=DIRECTION ( 'NONE',  ( -1.000000000000000000, 0.000000000000000000, 0.000000000000000000 ) ) ;
#4929=DIRECTION ( 'NONE',  ( 1.000000000000000000, 0.000000000000000000, 0.000000000000000000 ) ) ;
#4936=DIRECTION ( 'NONE',  ( 0.000000000000000000, -0.7071067811865473507, -0.7071067811865477948 ) ) ;
#4937=EDGE_CURVE ( 'NONE', #5417, #550, #2615, .T. ) ;
#4947=AXIS2_PLACEMENT_3D ( 'NONE', #9317, #6314, #5587 ) ;
#4949=ORIENTED_EDGE ( 'NONE', *, *, #8121, .F. ) ;
#4952=CYLINDRICAL_SURFACE ( 'NONE', #5361, 3.000000000000002665 ) ;
#4963=AXIS2_PLACEMENT_3D ( 'NONE', #5376, #319, #3203 ) ;
#4965=CARTESIAN_POINT ( 'NONE',  ( -15.99999999999999645, 43.00000000000000000, 11.99999999999999645 ) ) ;
#4968=ORIENTED_EDGE ( 'NONE', *, *, #7942, .T. ) ;
#4973=AXIS2_PLACEMENT_3D ( 'NONE', #512, #9249, #7188 ) ;
#4982=ORIENTED_EDGE ( 'NONE', *, *, #3603, .F. ) ;
#4986=CARTESIAN_POINT ( 'NONE',  ( -53.29490495164537833, -30.00000000000000000, -100.0000000000000000 ) ) ;
#4987=( BOUNDED_CURVE ( )  B_SPLINE_CURVE ( 3, ( #1876, #7101, #1198, #5627 ),
 .UNSPECIFIED., .F., .T. ) 
 B_SPLINE_CURVE_WITH_KNOTS ( ( 4, 4 ),
 ( 3.233473586661879118, 3.279793965437967973 ),
 .UNSPECIFIED. ) 
 CURVE ( )  GEOMETRIC_REPRESENTATION_ITEM ( )  RATIONAL_B_SPLINE_CURVE ( ( 1.000000000000000000, 0.9998212098678860293, 0.9998212098678860293, 1.000000000000000000 ) ) 
 REPRESENTATION_ITEM ( '' )  );
#4988=CARTESIAN_POINT ( 'NONE',  ( -50.79490495164537833, 29.99999999999999645, -82.50000000000000000 ) ) ;
#4992=ORIENTED_EDGE ( 'NONE', *, *, #3239, .T. ) ;
#4994=EDGE_CURVE ( 'NONE', #7343, #6251, #5809, .T. ) ;
#4995=VERTEX_POINT ( 'NONE', #1490 ) ;
#4999=ADVANCED_FACE ( 'NONE', ( #9171 ), #5904, .T. ) ;
#5000=DIRECTION ( 'NONE',  ( -1.000000000000000000, 0.000000000000000000, 0.000000000000000000 ) ) ;
#5002=DIRECTION ( 'NONE',  ( -1.000000000000000000, 0.000000000000000000, 0.000000000000000000 ) ) ;
#5009=DIRECTION ( 'NONE',  ( -1.000000000000000000, 0.000000000000000000, 0.000000000000000000 ) ) ;
#5014=VECTOR ( 'NONE', #5009, 1000.000000000000000 ) ;
#5015=EDGE_CURVE ( 'NONE', #55, #4223, #6834, .T. ) ;
#5017=VECTOR ( 'NONE', #7884, 1000.000000000000000 ) ;
#5023=EDGE_CURVE ( 'NONE', #1684, #8859, #4716, .T. ) ;
#5025=DIRECTION ( 'NONE',  ( 0.000000000000000000, 0.000000000000000000, 1.000000000000000000 ) ) ;
#5027=ORIENTED_EDGE ( 'NONE', *, *, #2259, .T. ) ;
#5029=DIRECTION ( 'NONE',  ( -0.000000000000000000, -0.000000000000000000, -1.000000000000000000 ) ) ;
#5030=CYLINDRICAL_SURFACE ( 'NONE', #3620, 7.250000000000002665 ) ;
#5031=VECTOR ( 'NONE', #6490, 1000.000000000000000 ) ;
#5035=DIRECTION ( 'NONE',  ( -0.6785983445458477759, 0.2810846377148170649, 0.6785983445458477759 ) ) ;
#5043=VECTOR ( 'NONE', #7051, 1000.000000000000000 ) ;
#5047=ORIENTED_EDGE ( 'NONE', *, *, #4414, .T. ) ;
#5060=EDGE_LOOP ( 'NONE', ( #4029, #3650, #3490, #2374 ) ) ;
#5061=FACE_BOUND ( 'NONE', #6169, .T. ) ;
#5064=CARTESIAN_POINT ( 'NONE',  ( -38.00000000000000711, 43.00000000000000000, 11.99999999999999645 ) ) ;
#5066=DIRECTION ( 'NONE',  ( 0.000000000000000000, 0.000000000000000000, 1.000000000000000000 ) ) ;
#5067=ORIENTED_EDGE ( 'NONE', *, *, #3950, .F. ) ;
#5070=ORIENTED_EDGE ( 'NONE', *, *, #1426, .T. ) ;
#5072=CARTESIAN_POINT ( 'NONE',  ( 60.00000000000000000, -3.673940397442057600E-15, -70.00000000000000000 ) ) ;
#5074=DIRECTION ( 'NONE',  ( 0.000000000000000000, 0.000000000000000000, -1.000000000000000000 ) ) ;
#5075=DIRECTION ( 'NONE',  ( 0.5773502691896253980, -0.000000000000000000, 0.8164965809277263675 ) ) ;
#5077=VECTOR ( 'NONE', #9140, 1000.000000000000000 ) ;
#5083=LINE ( 'NONE', #5130, #5031 ) ;
#5084=CARTESIAN_POINT ( 'NONE',  ( 52.83333333333332860, 1.666666666666670515, -110.8333333333333570 ) ) ;
#5085=CARTESIAN_POINT ( 'NONE',  ( 26.21170834203230982, 53.97171801779368394, -2.612255525622733554 ) ) ;
#5088=VERTEX_POINT ( 'NONE', #1099 ) ;
#5090=VERTEX_POINT ( 'NONE', #1689 ) ;
#5095=CARTESIAN_POINT ( 'NONE',  ( 60.00000000000000000, 15.90990257669733943, -82.90990257669729147 ) ) ;
#5099=ORIENTED_EDGE ( 'NONE', *, *, #7362, .T. ) ;
#5100=CARTESIAN_POINT ( 'NONE',  ( 53.29490495164537833, 15.90990257669733943, -85.90990257669729147 ) ) ;
#5110=VERTEX_POINT ( 'NONE', #5392 ) ;
#5111=ORIENTED_EDGE ( 'NONE', *, *, #1341, .F. ) ;
#5112=CARTESIAN_POINT ( 'NONE',  ( -57.72192878071321331, 19.00148731544555147, -33.94573509506509623 ) ) ;
#5114=DIRECTION ( 'NONE',  ( -0.000000000000000000, -0.000000000000000000, 1.000000000000000000 ) ) ;
#5121=LINE ( 'NONE', #7376, #3439 ) ;
#5123=ORIENTED_EDGE ( 'NONE', *, *, #153, .T. ) ;
#5126=CARTESIAN_POINT ( 'NONE',  ( -37.00000000000000711, 15.90990257669733943, -57.09009742330271564 ) ) ;
#5128=VECTOR ( 'NONE', #2718, 1000.000000000000000 ) ;
#5129=EDGE_CURVE ( 'NONE', #550, #18, #5133, .T. ) ;
#5130=CARTESIAN_POINT ( 'NONE',  ( 37.00000000000000000, -30.00000000000000000, -95.00000000000000000 ) ) ;
#5133=CIRCLE ( 'NONE', #5452, 11.00000000000000711 ) ;
#5134=CARTESIAN_POINT ( 'NONE',  ( -37.00000000000000000, -30.00000000000000000, -95.00000000000000000 ) ) ;
#5135=CARTESIAN_POINT ( 'NONE',  ( -53.29490495164537833, 15.90990257669733943, -57.09009742330271564 ) ) ;
#5137=ORIENTED_EDGE ( 'NONE', *, *, #8055, .T. ) ;
#5138=EDGE_LOOP ( 'NONE', ( #1790, #1231, #7102, #2335 ) ) ;
#5140=ORIENTED_EDGE ( 'NONE', *, *, #8741, .F. ) ;
#5142=CARTESIAN_POINT ( 'NONE',  ( 37.00000000000000000, 15.90990257669733943, -85.90990257669729147 ) ) ;
#5146=DIRECTION ( 'NONE',  ( 0.000000000000000000, 0.7071067811865473507, 0.7071067811865477948 ) ) ;
#5151=VECTOR ( 'NONE', #3580, 999.9999999999998863 ) ;
#5153=DIRECTION ( 'NONE',  ( -0.000000000000000000, -0.000000000000000000, -1.000000000000000000 ) ) ;
#5159=EDGE_CURVE ( 'NONE', #5946, #8372, #2689, .T. ) ;
#5160=ORIENTED_EDGE ( 'NONE', *, *, #4418, .T. ) ;
#5163=CARTESIAN_POINT ( 'NONE',  ( 60.00000000000000000, 15.90990257669733943, -85.90990257669729147 ) ) ;
#5164=CARTESIAN_POINT ( 'NONE',  ( -53.29490495164537833, -27.56180520566615044, -134.0000000000000284 ) ) ;
#5168=DIRECTION ( 'NONE',  ( 0.000000000000000000, 0.000000000000000000, 1.000000000000000000 ) ) ;
#5185=FACE_OUTER_BOUND ( 'NONE', #1136, .T. ) ;
#5186=ORIENTED_EDGE ( 'NONE', *, *, #6271, .F. ) ;
#5190=LINE ( 'NONE', #4374, #959 ) ;
#5198=CARTESIAN_POINT ( 'NONE',  ( 37.00000000000000000, -30.00000000000000000, -13.00000000000001066 ) ) ;
#5203=EDGE_LOOP ( 'NONE', ( #2676, #6036, #8389, #8295 ) ) ;
#5212=EDGE_LOOP ( 'NONE', ( #9205, #2535, #7010, #6110 ) ) ;
#5216=AXIS2_PLACEMENT_3D ( 'NONE', #101, #8077, #2364 ) ;
#5217=DIRECTION ( 'NONE',  ( 0.000000000000000000, -0.7071067811865479058, 0.7071067811865472397 ) ) ;
#5218=DIRECTION ( 'NONE',  ( 0.000000000000000000, 0.000000000000000000, 1.000000000000000000 ) ) ;
#5225=DIRECTION ( 'NONE',  ( 0.7071067811865463515, 0.5000000000000006661, 0.5000000000000012212 ) ) ;
#5227=ORIENTED_EDGE ( 'NONE', *, *, #7020, .F. ) ;
#5228=EDGE_CURVE ( 'NONE', #3211, #6868, #7829, .T. ) ;
#5230=AXIS2_PLACEMENT_3D ( 'NONE', #4354, #5710, #5800 ) ;
#5231=CARTESIAN_POINT ( 'NONE',  ( 37.00000000000000000, -13.96446609406729067, -95.00000000000000000 ) ) ;
#5239=DIRECTION ( 'NONE',  ( -1.000000000000000000, -0.000000000000000000, -0.000000000000000000 ) ) ;
#5243=EDGE_CURVE ( 'NONE', #4363, #9426, #2210, .T. ) ;
#5246=CARTESIAN_POINT ( 'NONE',  ( 26.21170834203229916, -53.97171801779367684, 11.99999999999999645 ) ) ;
#5250=( BOUNDED_CURVE ( )  B_SPLINE_CURVE ( 3, ( #9192, #4742, #1855, #8386 ),
 .UNSPECIFIED., .F., .F. ) 
 B_SPLINE_CURVE_WITH_KNOTS ( ( 4, 4 ),
 ( 5.235987755982988823, 5.613918313269388172 ),
 .UNSPECIFIED. ) 
 CURVE ( )  GEOMETRIC_REPRESENTATION_ITEM ( )  RATIONAL_B_SPLINE_CURVE ( ( 1.000000000000000000, 0.9881327504826167285, 0.9881327504826167285, 1.000000000000000000 ) ) 
 REPRESENTATION_ITEM ( '' )  );
#5251=ORIENTED_EDGE ( 'NONE', *, *, #3518, .T. ) ;
#5263=EDGE_LOOP ( 'NONE', ( #7297, #8211, #9013, #8649 ) ) ;
#5268=DIRECTION ( 'NONE',  ( -1.000000000000000000, 0.000000000000000000, 0.000000000000000000 ) ) ;
#5271=DIRECTION ( 'NONE',  ( 0.000000000000000000, 0.000000000000000000, 1.000000000000000000 ) ) ;
#5272=DIRECTION ( 'NONE',  ( -0.000000000000000000, -0.000000000000000000, -1.000000000000000000 ) ) ;
#5276=ORIENTED_EDGE ( 'NONE', *, *, #6305, .T. ) ;
#5277=ORIENTED_EDGE ( 'NONE', *, *, #2068, .F. ) ;
#5285=FACE_OUTER_BOUND ( 'NONE', #4734, .T. ) ;
#5286=ORIENTED_EDGE ( 'NONE', *, *, #913, .T. ) ;
#5287=ORIENTED_EDGE ( 'NONE', *, *, #4829, .T. ) ;
#5289=CARTESIAN_POINT ( 'NONE',  ( 16.00000000000000000, 43.00000000000000000, 11.99999999999999645 ) ) ;
#5294=DIRECTION ( 'NONE',  ( -1.000000000000000000, 0.000000000000000000, 0.000000000000000000 ) ) ;
#5298=ORIENTED_EDGE ( 'NONE', *, *, #137, .F. ) ;
#5299=EDGE_CURVE ( 'NONE', #8340, #2574, #41, .T. ) ;
#5302=ORIENTED_EDGE ( 'NONE', *, *, #8911, .F. ) ;
#5303=DIRECTION ( 'NONE',  ( 0.000000000000000000, 0.7071067811865479058, -0.7071067811865472397 ) ) ;
#5308=ORIENTED_EDGE ( 'NONE', *, *, #6671, .T. ) ;
#5309=VERTEX_POINT ( 'NONE', #6664 ) ;
#5311=ORIENTED_EDGE ( 'NONE', *, *, #3408, .T. ) ;
#5312=ORIENTED_EDGE ( 'NONE', *, *, #1009, .F. ) ;
#5318=VECTOR ( 'NONE', #960, 1000.000000000000000 ) ;
#5320=ADVANCED_FACE ( 'NONE', ( #8106 ), #790, .T. ) ;
#5321=CARTESIAN_POINT ( 'NONE',  ( 38.00000000000000000, -43.00000000000000000, 11.99999999999999645 ) ) ;
#5324=ORIENTED_EDGE ( 'NONE', *, *, #5023, .F. ) ;
#5325=CYLINDRICAL_SURFACE ( 'NONE', #3607, 3.000000000000002665 ) ;
#5333=VECTOR ( 'NONE', #8032, 999.9999999999998863 ) ;
#5337=AXIS2_PLACEMENT_3D ( 'NONE', #2344, #8248, #9057 ) ;
#5341=AXIS2_PLACEMENT_3D ( 'NONE', #3543, #9404, #6931 ) ;
#5344=CARTESIAN_POINT ( 'NONE',  ( 37.22467645238197775, 47.05659850664388699, -0.5000000000000038858 ) ) ;
#5349=DIRECTION ( 'NONE',  ( 0.000000000000000000, 0.000000000000000000, 1.000000000000000000 ) ) ;
#5352=ORIENTED_EDGE ( 'NONE', *, *, #6134, .T. ) ;
#5353=DIRECTION ( 'NONE',  ( 0.000000000000000000, 0.000000000000000000, -1.000000000000000000 ) ) ;
#5355=ORIENTED_EDGE ( 'NONE', *, *, #657, .F. ) ;
#5356=DIRECTION ( 'NONE',  ( 0.000000000000000000, -0.000000000000000000, 1.000000000000000000 ) ) ;
#5359=DIRECTION ( 'NONE',  ( 0.000000000000000000, 0.000000000000000000, 1.000000000000000000 ) ) ;
#5360=VECTOR ( 'NONE', #1179, 1000.000000000000000 ) ;
#5361=AXIS2_PLACEMENT_3D ( 'NONE', #2073, #5002, #3560 ) ;
#5366=ORIENTED_EDGE ( 'NONE', *, *, #8658, .T. ) ;
#5369=DIRECTION ( 'NONE',  ( -0.6785983445458484420, -0.2810846377148113473, -0.6785983445458493302 ) ) ;
#5371=EDGE_CURVE ( 'NONE', #3861, #8166, #8912, .T. ) ;
#5373=DIRECTION ( 'NONE',  ( -0.000000000000000000, -0.000000000000000000, -1.000000000000000000 ) ) ;
#5375=CARTESIAN_POINT ( 'NONE',  ( 37.00000000000000000, -8.017766952966344007, -116.9822330470336453 ) ) ;
#5376=CARTESIAN_POINT ( 'NONE',  ( 37.00000000000000000, 15.90990257669733943, -54.09009742330271564 ) ) ;
#5383=EDGE_LOOP ( 'NONE', ( #755, #8535, #2984, #9126, #5685, #9286, #923, #7225, #1630, #5646, #6987, #5311, #6678, #1245, #8569, #718, #9199, #8659, #1303, #8900 ) ) ;
#5391=DIRECTION ( 'NONE',  ( 0.000000000000000000, 0.000000000000000000, 1.000000000000000000 ) ) ;
#5392=CARTESIAN_POINT ( 'NONE',  ( 53.29490495164537833, -1.836970198721028011E-15, -85.00000000000000000 ) ) ;
#5396=AXIS2_PLACEMENT_3D ( 'NONE', #9191, #2628, #5558 ) ;
#5397=ORIENTED_EDGE ( 'NONE', *, *, #8229, .F. ) ;
#5402=CARTESIAN_POINT ( 'NONE',  ( 27.00000000000000000, -43.00000000000000000, 11.99999999999999645 ) ) ;
#5415=ORIENTED_EDGE ( 'NONE', *, *, #5960, .F. ) ;
#5417=VERTEX_POINT ( 'NONE', #7521 ) ;
#5421=FACE_BOUND ( 'NONE', #6223, .T. ) ;
#5424=EDGE_CURVE ( 'NONE', #1561, #472, #4515, .T. ) ;
#5425=ORIENTED_EDGE ( 'NONE', *, *, #7216, .F. ) ;
#5438=CARTESIAN_POINT ( 'NONE',  ( 60.00000000000000000, -15.90990257669733943, -85.90990257669729147 ) ) ;
#5443=AXIS2_PLACEMENT_3D ( 'NONE', #240, #8452, #4561 ) ;
#5444=CARTESIAN_POINT ( 'NONE',  ( 37.00000000000000000, -15.90990257669733943, -51.09009742330271564 ) ) ;
#5446=CARTESIAN_POINT ( 'NONE',  ( -26.21170834203229205, -53.97171801779368394, 11.99999999999999645 ) ) ;
#5448=CARTESIAN_POINT ( 'NONE',  ( 37.00000000000000000, 30.00000000000000000, -95.00000000000000000 ) ) ;
#5452=AXIS2_PLACEMENT_3D ( 'NONE', #4039, #7591, #3221 ) ;
#5455=ORIENTED_EDGE ( 'NONE', *, *, #1752, .F. ) ;
#5456=CARTESIAN_POINT ( 'NONE',  ( 60.00000000000000000, 7.347880794884118356E-15, -30.00000000000000000 ) ) ;
#5458=CARTESIAN_POINT ( 'NONE',  ( -53.29490495164537833, 11.46446609406724626, -97.50000000000000000 ) ) ;
#5466=ORIENTED_EDGE ( 'NONE', *, *, #2717, .T. ) ;
#5467=DIRECTION ( 'NONE',  ( -1.000000000000000000, 0.000000000000000000, 0.000000000000000000 ) ) ;
#5468=ORIENTED_EDGE ( 'NONE', *, *, #1426, .F. ) ;
#5473=DIRECTION ( 'NONE',  ( -0.000000000000000000, -0.000000000000000000, 1.000000000000000000 ) ) ;
#5484=AXIS2_PLACEMENT_3D ( 'NONE', #6581, #4411, #2199 ) ;
#5488=CARTESIAN_POINT ( 'NONE',  ( -27.00000000000000000, 43.00000000000000000, -25.00000000000000000 ) ) ;
#5500=LINE ( 'NONE', #1743, #1247 ) ;
#5502=EDGE_LOOP ( 'NONE', ( #8876, #3133, #3111, #3159, #5324 ) ) ;
#5503=ORIENTED_EDGE ( 'NONE', *, *, #6602, .F. ) ;
#5504=DIRECTION ( 'NONE',  ( 0.000000000000000000, 0.000000000000000000, 1.000000000000000000 ) ) ;
#5506=CARTESIAN_POINT ( 'NONE',  ( 53.29490495164537833, -15.90990257669733943, -57.09009742330271564 ) ) ;
#5507=CARTESIAN_POINT ( 'NONE',  ( -53.29490495164537833, -30.00000000000000000, -97.50000000000000000 ) ) ;
#5508=AXIS2_PLACEMENT_3D ( 'NONE', #4491, #836, #3770 ) ;
#5513=LINE ( 'NONE', #1219, #9410 ) ;
#5515=VERTEX_POINT ( 'NONE', #6992 ) ;
#5519=CARTESIAN_POINT ( 'NONE',  ( -50.79490495164537833, -30.00000000000000355, -82.50000000000001421 ) ) ;
#5520=ORIENTED_EDGE ( 'NONE', *, *, #2125, .F. ) ;
#5526=ORIENTED_EDGE ( 'NONE', *, *, #9026, .T. ) ;
#5531=DIRECTION ( 'NONE',  ( 0.000000000000000000, -0.7071067811865473507, -0.7071067811865477948 ) ) ;
#5538=AXIS2_PLACEMENT_3D ( 'NONE', #5992, #5938, #5218 ) ;
#5542=EDGE_CURVE ( 'NONE', #4079, #2481, #5250, .T. ) ;
#5544=DIRECTION ( 'NONE',  ( -1.000000000000000000, 0.000000000000000000, 0.000000000000000000 ) ) ;
#5555=ADVANCED_FACE ( 'NONE', ( #318 ), #9097, .F. ) ;
#5556=CARTESIAN_POINT ( 'NONE',  ( 60.00000000000000000, -30.00000000000000355, -82.50000000000001421 ) ) ;
#5558=DIRECTION ( 'NONE',  ( 0.000000000000000000, 0.000000000000000000, 1.000000000000000000 ) ) ;
#5564=( BOUNDED_CURVE ( )  B_SPLINE_CURVE ( 3, ( #7657, #1843, #1071, #4007 ),
 .UNSPECIFIED., .F., .T. ) 
 B_SPLINE_CURVE_WITH_KNOTS ( ( 4, 4 ),
 ( 5.235987755982987935, 5.613918313269388172 ),
 .UNSPECIFIED. ) 
 CURVE ( )  GEOMETRIC_REPRESENTATION_ITEM ( )  RATIONAL_B_SPLINE_CURVE ( ( 1.000000000000000000, 0.9881327504826167285, 0.9881327504826167285, 1.000000000000000000 ) ) 
 REPRESENTATION_ITEM ( '' )  );
#5565=CYLINDRICAL_SURFACE ( 'NONE', #7308, 7.250000000000002665 ) ;
#5571=CYLINDRICAL_SURFACE ( 'NONE', #8225, 11.00000000000000711 ) ;
#5572=DIRECTION ( 'NONE',  ( -0.000000000000000000, -0.000000000000000000, -1.000000000000000000 ) ) ;
#5574=DIRECTION ( 'NONE',  ( 0.000000000000000000, 0.000000000000000000, -1.000000000000000000 ) ) ;
#5575=CARTESIAN_POINT ( 'NONE',  ( -26.21170834203230982, -53.97171801779368394, -2.612255525622733554 ) ) ;
#5581=CARTESIAN_POINT ( 'NONE',  ( -27.00000000000000000, -43.00000000000000000, 11.99999999999999645 ) ) ;
#5586=ORIENTED_EDGE ( 'NONE', *, *, #156, .F. ) ;
#5587=DIRECTION ( 'NONE',  ( 0.000000000000000000, 0.000000000000000000, 1.000000000000000000 ) ) ;
#5588=DIRECTION ( 'NONE',  ( -1.000000000000000000, 0.000000000000000000, 0.000000000000000000 ) ) ;
#5594=PLANE ( 'NONE',  #1036 ) ;
#5603=DIRECTION ( 'NONE',  ( 0.000000000000000000, 0.000000000000000000, -1.000000000000000000 ) ) ;
#5609=VERTEX_POINT ( 'NONE', #3428 ) ;
#5611=EDGE_CURVE ( 'NONE', #4522, #2905, #3571, .T. ) ;
#5614=LINE ( 'NONE', #3347, #5043 ) ;
#5615=CARTESIAN_POINT ( 'NONE',  ( 27.00000000000000000, 43.00000000000000000, 11.99999999999999645 ) ) ;
#5618=( BOUNDED_CURVE ( )  B_SPLINE_CURVE ( 3, ( #1548, #5978, #7406, #8181 ),
 .UNSPECIFIED., .F., .F. ) 
 B_SPLINE_CURVE_WITH_KNOTS ( ( 4, 4 ),
 ( 4.712388980384689674, 7.853981633974482790 ),
 .UNSPECIFIED. ) 
 CURVE ( )  GEOMETRIC_REPRESENTATION_ITEM ( )  RATIONAL_B_SPLINE_CURVE ( ( 1.000000000000000000, 0.3333333333333333703, 0.3333333333333333703, 1.000000000000000000 ) ) 
 REPRESENTATION_ITEM ( '' )  );
#5619=CARTESIAN_POINT ( 'NONE',  ( -60.00000000000000000, 0.000000000000000000, 23.99999999999998579 ) ) ;
#5627=CARTESIAN_POINT ( 'NONE',  ( -53.29490495164537833, 27.56180520566615044, -81.40266088840108694 ) ) ;
#5628=EDGE_LOOP ( 'NONE', ( #9100, #8831, #2098, #4200 ) ) ;
#5637=EDGE_CURVE ( 'NONE', #2574, #4808, #1363, .T. ) ;
#5639=CARTESIAN_POINT ( 'NONE',  ( -53.29490495164537833, -15.90990257669733943, -85.90990257669729147 ) ) ;
#5646=ORIENTED_EDGE ( 'NONE', *, *, #3834, .T. ) ;
#5649=VECTOR ( 'NONE', #4936, 999.9999999999998863 ) ;
#5650=AXIS2_PLACEMENT_3D ( 'NONE', #444, #1156, #5544 ) ;
#5657=EDGE_CURVE ( 'NONE', #975, #3514, #7127, .T. ) ;
#5658=ORIENTED_EDGE ( 'NONE', *, *, #4715, .F. ) ;
#5660=VERTEX_POINT ( 'NONE', #4919 ) ;
#5662=EDGE_CURVE ( 'NONE', #3407, #1534, #1282, .T. ) ;
#5663=DIRECTION ( 'NONE',  ( -0.7071067811865470176, 0.000000000000000000, -0.7071067811865481278 ) ) ;
#5664=AXIS2_PLACEMENT_3D ( 'NONE', #6382, #9291, #2729 ) ;
#5679=EDGE_CURVE ( 'NONE', #4271, #1738, #597, .T. ) ;
#5680=DIRECTION ( 'NONE',  ( -1.000000000000000000, 0.000000000000000000, -0.000000000000000000 ) ) ;
#5681=DIRECTION ( 'NONE',  ( 1.000000000000000000, 0.000000000000000000, 0.000000000000000000 ) ) ;
#5683=VERTEX_POINT ( 'NONE', #7994 ) ;
#5685=ORIENTED_EDGE ( 'NONE', *, *, #8922, .T. ) ;
#5691=ORIENTED_EDGE ( 'NONE', *, *, #7963, .T. ) ;
#5694=VERTEX_POINT ( 'NONE', #7220 ) ;
#5706=CARTESIAN_POINT ( 'NONE',  ( -60.00000000000000000, 30.00000000000000000, -13.00000000000000000 ) ) ;
#5708=LINE ( 'NONE', #7229, #5151 ) ;
#5710=DIRECTION ( 'NONE',  ( -0.000000000000000000, -0.000000000000000000, 1.000000000000000000 ) ) ;
#5717=EDGE_CURVE ( 'NONE', #3765, #4223, #36, .T. ) ;
#5719=AXIS2_PLACEMENT_3D ( 'NONE', #865, #1443, #2980 ) ;
#5724=CARTESIAN_POINT ( 'NONE',  ( 60.00000000000000000, -15.90990257669733943, -82.90990257669729147 ) ) ;
#5734=CARTESIAN_POINT ( 'NONE',  ( 41.99999999999999289, 12.50000000000000355, -100.0000000000000000 ) ) ;
#5736=ADVANCED_FACE ( 'NONE', ( #4483 ), #3763, .F. ) ;
#5742=ORIENTED_EDGE ( 'NONE', *, *, #3413, .F. ) ;
#5746=DIRECTION ( 'NONE',  ( -1.000000000000000000, 0.000000000000000000, 0.000000000000000000 ) ) ;
#5755=CIRCLE ( 'NONE', #6669, 3.000000000000002665 ) ;
#5757=FACE_OUTER_BOUND ( 'NONE', #88, .T. ) ;
#5763=EDGE_LOOP ( 'NONE', ( #5352, #7926 ) ) ;
#5765=LINE ( 'NONE', #1277, #4721 ) ;
#5772=EDGE_CURVE ( 'NONE', #6722, #4478, #3046, .T. ) ;
#5775=DIRECTION ( 'NONE',  ( -1.000000000000000000, -0.000000000000000000, -0.000000000000000000 ) ) ;
#5789=DIRECTION ( 'NONE',  ( 1.000000000000000000, -0.000000000000000000, -0.000000000000000000 ) ) ;
#5794=VECTOR ( 'NONE', #3831, 1000.000000000000000 ) ;
#5799=DIRECTION ( 'NONE',  ( -0.000000000000000000, -0.000000000000000000, 1.000000000000000000 ) ) ;
#5800=DIRECTION ( 'NONE',  ( -1.000000000000000000, 0.000000000000000000, 0.000000000000000000 ) ) ;
#5801=AXIS2_PLACEMENT_3D ( 'NONE', #2546, #3990, #6779 ) ;
#5804=VERTEX_POINT ( 'NONE', #6797 ) ;
#5808=AXIS2_PLACEMENT_3D ( 'NONE', #3098, #6037, #2386 ) ;
#5809=CIRCLE ( 'NONE', #5216, 60.00000000000000000 ) ;
#5814=EDGE_CURVE ( 'NONE', #8237, #523, #8898, .T. ) ;
#5818=DIRECTION ( 'NONE',  ( 0.000000000000000000, 0.000000000000000000, -1.000000000000000000 ) ) ;
#5819=CARTESIAN_POINT ( 'NONE',  ( -27.00000000000000000, 43.00000000000000000, 11.99999999999999645 ) ) ;
#5824=EDGE_CURVE ( 'NONE', #4881, #1684, #7411, .T. ) ;
#5827=ADVANCED_FACE ( 'NONE', ( #5927 ), #8854, .F. ) ;
#5828=FACE_OUTER_BOUND ( 'NONE', #2097, .T. ) ;
#5832=PLANE ( 'NONE',  #350 ) ;
#5834=CARTESIAN_POINT ( 'NONE',  ( 53.29490495164537833, -15.90990257669733943, -82.90990257669729147 ) ) ;
#5836=DIRECTION ( 'NONE',  ( 0.000000000000000000, 1.000000000000000000, 0.000000000000000000 ) ) ;
#5845=FACE_OUTER_BOUND ( 'NONE', #1592, .T. ) ;
#5855=PRODUCT ( '3-Flange Yoke', '3-Flange Yoke', '', ( #1056 ) ) ;
#5859=VERTEX_POINT ( 'NONE', #8951 ) ;
#5860=ORIENTED_EDGE ( 'NONE', *, *, #2807, .F. ) ;
#5870=AXIS2_PLACEMENT_3D ( 'NONE', #3136, #7598, #4627 ) ;
#5881=EDGE_CURVE ( 'NONE', #4256, #5932, #3337, .T. ) ;
#5882=DIRECTION ( 'NONE',  ( -1.000000000000000000, 0.000000000000000000, 0.000000000000000000 ) ) ;
#5888=LINE ( 'NONE', #5934, #1057 ) ;
#5891=LINE ( 'NONE', #5936, #4397 ) ;
#5893=CARTESIAN_POINT ( 'NONE',  ( -37.00000000000000711, -3.673940397442057600E-15, -70.00000000000000000 ) ) ;
#5894=CYLINDRICAL_SURFACE ( 'NONE', #7123, 60.00000000000000000 ) ;
#5895=DIRECTION ( 'NONE',  ( 0.000000000000000000, 0.000000000000000000, 1.000000000000000000 ) ) ;
#5901=ORIENTED_EDGE ( 'NONE', *, *, #1430, .F. ) ;
#5904=CONICAL_SURFACE ( 'NONE', #7896, 59.00000000000000000, 0.7853981633974415066 ) ;
#5911=DIRECTION ( 'NONE',  ( 0.000000000000000000, 1.000000000000000000, 0.000000000000000000 ) ) ;
#5912=DIRECTION ( 'NONE',  ( -0.000000000000000000, -0.000000000000000000, -1.000000000000000000 ) ) ;
#5917=CYLINDRICAL_SURFACE ( 'NONE', #1960, 11.00000000000000711 ) ;
#5918=( BOUNDED_CURVE ( )  B_SPLINE_CURVE ( 3, ( #1479, #8829, #8882, #8016 ),
 .UNSPECIFIED., .F., .T. ) 
 B_SPLINE_CURVE_WITH_KNOTS ( ( 4, 4 ),
 ( 5.805906910357376383, 6.283185307179586232 ),
 .UNSPECIFIED. ) 
 CURVE ( )  GEOMETRIC_REPRESENTATION_ITEM ( )  RATIONAL_B_SPLINE_CURVE ( ( 1.000000000000000000, 0.9811070276743185659, 0.9811070276743185659, 1.000000000000000000 ) ) 
 REPRESENTATION_ITEM ( '' )  );
#5927=FACE_OUTER_BOUND ( 'NONE', #1545, .T. ) ;
#5928=CIRCLE ( 'NONE', #7919, 7.250000000000002665 ) ;
#5932=VERTEX_POINT ( 'NONE', #2477 ) ;
#5933=ADVANCED_FACE ( 'NONE', ( #3189 ), #2519, .F. ) ;
#5934=CARTESIAN_POINT ( 'NONE',  ( 60.00000000000000000, -15.90990257669733943, -51.09009742330271564 ) ) ;
#5936=CARTESIAN_POINT ( 'NONE',  ( 53.29490495164537833, 27.56180520566615044, -134.0000000000000284 ) ) ;
#5938=DIRECTION ( 'NONE',  ( -1.000000000000000000, 0.000000000000000000, 0.000000000000000000 ) ) ;
#5944=VERTEX_POINT ( 'NONE', #1698 ) ;
#5946=VERTEX_POINT ( 'NONE', #261 ) ;
#5948=EDGE_CURVE ( 'NONE', #2323, #4692, #4053, .T. ) ;
#5952=LINE ( 'NONE', #7432, #8258 ) ;
#5953=CIRCLE ( 'NONE', #1807, 3.000000000000002665 ) ;
#5955=FACE_OUTER_BOUND ( 'NONE', #121, .T. ) ;
#5960=EDGE_CURVE ( 'NONE', #5995, #3553, #5500, .T. ) ;
#5962=EDGE_CURVE ( 'NONE', #7596, #580, #1788, .T. ) ;
#5967=CARTESIAN_POINT ( 'NONE',  ( 52.42476942962458963, 29.19763577280652811, -80.99738777760514097 ) ) ;
#5968=AXIS2_PLACEMENT_3D ( 'NONE', #8653, #6404, #4145 ) ;
#5974=VERTEX_POINT ( 'NONE', #2664 ) ;
#5975=AXIS2_PLACEMENT_3D ( 'NONE', #4773, #2425, #3906 ) ;
#5978=CARTESIAN_POINT ( 'NONE',  ( 15.99999999999999822, -21.00000000000000000, -16.89999999999999858 ) ) ;
#5979=CARTESIAN_POINT ( 'NONE',  ( -60.00000000000000000, 0.000000000000000000, 25.00000000000000000 ) ) ;
#5983=ORIENTED_EDGE ( 'NONE', *, *, #8544, .T. ) ;
#5987=CARTESIAN_POINT ( 'NONE',  ( 27.00000000000000000, 43.00000000000000000, 11.99999999999999645 ) ) ;
#5989=AXIS2_PLACEMENT_3D ( 'NONE', #2704, #7209, #8561 ) ;
#5992=CARTESIAN_POINT ( 'NONE',  ( -53.29490495164537833, -30.00000000000000000, -41.61356529332876875 ) ) ;
#5995=VERTEX_POINT ( 'NONE', #4682 ) ;
#5998=CARTESIAN_POINT ( 'NONE',  ( -20.14434505884620918, -53.53579249963524234, -2.801156583491396734 ) ) ;
#6000=EDGE_LOOP ( 'NONE', ( #4895, #2698, #8557, #4315 ) ) ;
#6001=DIRECTION ( 'NONE',  ( -0.5773502691896293948, -0.000000000000000000, -0.8164965809277234809 ) ) ;
#6004=EDGE_CURVE ( 'NONE', #3384, #1832, #5564, .T. ) ;
#6012=CARTESIAN_POINT ( 'NONE',  ( -53.29490495164537833, -3.673940397442057600E-15, -55.00000000000000711 ) ) ;
#6013=DIRECTION ( 'NONE',  ( 0.000000000000000000, -0.7071067811865473507, -0.7071067811865477948 ) ) ;
#6023=ORIENTED_EDGE ( 'NONE', *, *, #3633, .T. ) ;
#6036=ORIENTED_EDGE ( 'NONE', *, *, #6671, .F. ) ;
#6037=DIRECTION ( 'NONE',  ( 0.000000000000000000, 0.000000000000000000, 1.000000000000000000 ) ) ;
#6045=VERTEX_POINT ( 'NONE', #489 ) ;
#6046=LINE ( 'NONE', #3158, #8232 ) ;
#6050=ORIENTED_EDGE ( 'NONE', *, *, #1554, .T. ) ;
#6057=DIRECTION ( 'NONE',  ( -1.000000000000000000, 0.000000000000000000, 0.000000000000000000 ) ) ;
#6058=ORIENTED_EDGE ( 'NONE', *, *, #9056, .T. ) ;
#6062=DIRECTION ( 'NONE',  ( -1.000000000000000000, 0.000000000000000000, 0.000000000000000000 ) ) ;
#6063=DIRECTION ( 'NONE',  ( 0.7071067811865494601, -0.4999999999999988343, 0.4999999999999985012 ) ) ;
#6065=PRODUCT_DEFINITION_CONTEXT ( 'detailed design', #1678, 'design' ) ;
#6067=( NAMED_UNIT ( * ) PLANE_ANGLE_UNIT ( ) SI_UNIT ( $, .RADIAN. ) );
#6073=ORIENTED_EDGE ( 'NONE', *, *, #7823, .F. ) ;
#6076=CARTESIAN_POINT ( 'NONE',  ( 0.000000000000000000, 0.000000000000000000, 25.00000000000000000 ) ) ;
#6077=CARTESIAN_POINT ( 'NONE',  ( 53.29490495164537833, -15.90990257669733943, -54.09009742330271564 ) ) ;
#6081=EDGE_LOOP ( 'NONE', ( #2451, #2417, #3147, #7597, #7460, #4525, #9046, #2631, #7154, #7868, #8396, #6861, #2740, #4864, #7734, #6969, #6181, #5466, #8275, #2349 ) ) ;
#6101=( GEOMETRIC_REPRESENTATION_CONTEXT ( 3 ) GLOBAL_UNCERTAINTY_ASSIGNED_CONTEXT ( ( #3740 ) ) GLOBAL_UNIT_ASSIGNED_CONTEXT ( ( #8042, #2995, #8146 ) ) REPRESENTATION_CONTEXT ( 'NONE', 'WORKASPACE' ) );
#6102=ORIENTED_EDGE ( 'NONE', *, *, #4225, .F. ) ;
#6105=VECTOR ( 'NONE', #6934, 1000.000000000000000 ) ;
#6110=ORIENTED_EDGE ( 'NONE', *, *, #4300, .F. ) ;
#6114=DIRECTION ( 'NONE',  ( -0.000000000000000000, -0.000000000000000000, -1.000000000000000000 ) ) ;
#6115=DIRECTION ( 'NONE',  ( 0.000000000000000000, 0.000000000000000000, -1.000000000000000000 ) ) ;
#6118=DIRECTION ( 'NONE',  ( -1.000000000000000000, 0.000000000000000000, 0.000000000000000000 ) ) ;
#6120=ADVANCED_FACE ( 'NONE', ( #3561 ), #6405, .T. ) ;
#6124=VERTEX_POINT ( 'NONE', #8703 ) ;
#6128=EDGE_CURVE ( 'NONE', #313, #7585, #3279, .T. ) ;
#6130=VECTOR ( 'NONE', #6184, 1000.000000000000000 ) ;
#6133=ORIENTED_EDGE ( 'NONE', *, *, #8122, .T. ) ;
#6134=EDGE_CURVE ( 'NONE', #438, #5859, #3714, .T. ) ;
#6137=ORIENTED_EDGE ( 'NONE', *, *, #4011, .F. ) ;
#6140=LINE ( 'NONE', #3820, #2595 ) ;
#6145=CARTESIAN_POINT ( 'NONE',  ( -53.29490495164537833, -11.46446609406728179, -97.50000000000000000 ) ) ;
#6157=DIRECTION ( 'NONE',  ( 1.000000000000000000, 0.000000000000000000, -0.000000000000000000 ) ) ;
#6159=ORIENTED_EDGE ( 'NONE', *, *, #6220, .T. ) ;
#6160=EDGE_LOOP ( 'NONE', ( #3085, #8000 ) ) ;
#6169=EDGE_LOOP ( 'NONE', ( #9275, #7341 ) ) ;
#6175=ADVANCED_FACE ( 'NONE', ( #917 ), #7396, .F. ) ;
#6177=DIRECTION ( 'NONE',  ( 0.000000000000000000, 0.7071067811865473507, 0.7071067811865477948 ) ) ;
#6181=ORIENTED_EDGE ( 'NONE', *, *, #4113, .T. ) ;
#6184=DIRECTION ( 'NONE',  ( -0.000000000000000000, -0.000000000000000000, 1.000000000000000000 ) ) ;
#6186=CARTESIAN_POINT ( 'NONE',  ( 0.000000000000000000, 0.000000000000000000, 25.00000000000000000 ) ) ;
#6187=CARTESIAN_POINT ( 'NONE',  ( -37.22467645238203460, -47.05659850664382304, -5.608807313787673721 ) ) ;
#6189=CIRCLE ( 'NONE', #9395, 59.00000000000000000 ) ;
#6192=ORIENTED_EDGE ( 'NONE', *, *, #1615, .T. ) ;
#6193=DIRECTION ( 'NONE',  ( 0.000000000000000000, 0.000000000000000000, -1.000000000000000000 ) ) ;
#6196=FACE_BOUND ( 'NONE', #7561, .T. ) ;
#6197=ORIENTED_EDGE ( 'NONE', *, *, #9343, .F. ) ;
#6201=LINE ( 'NONE', #9022, #8195 ) ;
#6203=ORIENTED_EDGE ( 'NONE', *, *, #3975, .T. ) ;
#6204=ORIENTED_EDGE ( 'NONE', *, *, #4434, .T. ) ;
#6207=CARTESIAN_POINT ( 'NONE',  ( 51.96152422706632734, -30.00000000000000000, -80.85015119857384036 ) ) ;
#6219=DIRECTION ( 'NONE',  ( 0.000000000000000000, 0.000000000000000000, -1.000000000000000000 ) ) ;
#6220=EDGE_CURVE ( 'NONE', #4781, #2503, #8217, .T. ) ;
#6223=EDGE_LOOP ( 'NONE', ( #1450, #704 ) ) ;
#6227=CARTESIAN_POINT ( 'NONE',  ( -34.25000000000000000, -43.00000000000000000, 25.00000000000000000 ) ) ;
#6231=DIRECTION ( 'NONE',  ( -1.000000000000000000, 0.000000000000000000, 0.000000000000000000 ) ) ;
#6234=EDGE_CURVE ( 'NONE', #1975, #6538, #4030, .T. ) ;
#6238=CARTESIAN_POINT ( 'NONE',  ( 60.00000000000000000, 15.90990257669733943, -85.90990257669729147 ) ) ;
#6241=DIRECTION ( 'NONE',  ( -1.000000000000000000, 0.000000000000000000, 0.000000000000000000 ) ) ;
#6251=VERTEX_POINT ( 'NONE', #5246 ) ;
#6255=ADVANCED_FACE ( 'NONE', ( #1587 ), #770, .F. ) ;
#6260=DIRECTION ( 'NONE',  ( 1.000000000000000000, 0.000000000000000000, 0.000000000000000000 ) ) ;
#6263=EDGE_CURVE ( 'NONE', #8518, #8127, #3223, .T. ) ;
#6269=CARTESIAN_POINT ( 'NONE',  ( -53.29490495164537833, -27.56180520566615044, -81.40266088840114378 ) ) ;
#6270=VERTEX_POINT ( 'NONE', #6207 ) ;
#6271=EDGE_CURVE ( 'NONE', #4522, #7415, #1098, .T. ) ;
#6273=DIRECTION ( 'NONE',  ( 1.000000000000000000, 0.000000000000000000, 0.000000000000000000 ) ) ;
#6278=CARTESIAN_POINT ( 'NONE',  ( 53.29490495164537833, -27.56180520566615044, -134.0000000000000284 ) ) ;
#6279=VERTEX_POINT ( 'NONE', #1101 ) ;
#6282=ORIENTED_EDGE ( 'NONE', *, *, #753, .T. ) ;
#6288=CARTESIAN_POINT ( 'NONE',  ( -41.99999999999999289, -12.49999999999999645, -100.0000000000000000 ) ) ;
#6289=ORIENTED_EDGE ( 'NONE', *, *, #6758, .F. ) ;
#6290=VERTEX_POINT ( 'NONE', #7643 ) ;
#6294=CARTESIAN_POINT ( 'NONE',  ( -37.00000000000000711, 15.90990257669733943, -54.09009742330271564 ) ) ;
#6299=FACE_OUTER_BOUND ( 'NONE', #1073, .T. ) ;
#6305=EDGE_CURVE ( 'NONE', #367, #7733, #6974, .T. ) ;
#6310=ORIENTED_EDGE ( 'NONE', *, *, #2125, .T. ) ;
#6314=DIRECTION ( 'NONE',  ( 1.000000000000000000, -0.000000000000000000, -0.000000000000000000 ) ) ;
#6337=AXIS2_PLACEMENT_3D ( 'NONE', #4228, #8601, #6273 ) ;
#6342=ADVANCED_FACE ( 'NONE', ( #2466 ), #4086, .F. ) ;
#6344=AXIS2_PLACEMENT_3D ( 'NONE', #4241, #7038, #9329 ) ;
#6348=MANIFOLD_SOLID_BREP ( 'Pah3', #1644 ) ;
#6354=CARTESIAN_POINT ( 'NONE',  ( -38.00000000000000711, -43.00000000000000000, -7.366666666666667140 ) ) ;
#6355=DIRECTION ( 'NONE',  ( -1.000000000000000000, 0.000000000000000000, -0.000000000000000000 ) ) ;
#6364=AXIS2_PLACEMENT_3D ( 'NONE', #5893, #8818, #8152 ) ;
#6367=VERTEX_POINT ( 'NONE', #1572 ) ;
#6373=EDGE_CURVE ( 'NONE', #8783, #7512, #3832, .T. ) ;
#6382=CARTESIAN_POINT ( 'NONE',  ( 27.00000000000000000, -43.00000000000000000, 11.99999999999999645 ) ) ;
#6383=FACE_OUTER_BOUND ( 'NONE', #8708, .T. ) ;
#6393=DIRECTION ( 'NONE',  ( -0.000000000000000000, -0.000000000000000000, -1.000000000000000000 ) ) ;
#6394=VECTOR ( 'NONE', #5217, 999.9999999999998863 ) ;
#6396=CARTESIAN_POINT ( 'NONE',  ( 27.00000000000000000, 43.00000000000000000, -25.00000000000000000 ) ) ;
#6403=DIRECTION ( 'NONE',  ( -0.000000000000000000, -0.000000000000000000, -1.000000000000000000 ) ) ;
#6404=DIRECTION ( 'NONE',  ( 0.000000000000000000, 0.000000000000000000, -1.000000000000000000 ) ) ;
#6405=PLANE ( 'NONE',  #8771 ) ;
#6416=CIRCLE ( 'NONE', #4568, 7.250000000000002665 ) ;
#6419=ADVANCED_FACE ( 'NONE', ( #7335 ), #757, .F. ) ;
#6420=DIRECTION ( 'NONE',  ( -1.000000000000000000, 0.000000000000000000, 0.000000000000000000 ) ) ;
#6429=DIRECTION ( 'NONE',  ( 0.000000000000000000, 0.000000000000000000, 1.000000000000000000 ) ) ;
#6435=CARTESIAN_POINT ( 'NONE',  ( 16.00000000000000000, 43.00000000000000000, 11.99999999999999645 ) ) ;
#6437=CARTESIAN_POINT ( 'NONE',  ( 37.22467645238197775, -47.05659850664388699, -5.608807313787648852 ) ) ;
#6442=DIRECTION ( 'NONE',  ( 0.5773502691896281735, 0.000000000000000000, -0.8164965809277242581 ) ) ;
#6449=EDGE_LOOP ( 'NONE', ( #5520, #353, #537, #5366 ) ) ;
#6451=EDGE_LOOP ( 'NONE', ( #264, #4045, #7939, #2194 ) ) ;
#6453=EDGE_LOOP ( 'NONE', ( #7811, #3623, #9136, #1714 ) ) ;
#6455=FACE_OUTER_BOUND ( 'NONE', #1700, .T. ) ;
#6456=DIRECTION ( 'NONE',  ( -0.000000000000000000, -0.000000000000000000, -1.000000000000000000 ) ) ;
#6461=ORIENTED_EDGE ( 'NONE', *, *, #7768, .F. ) ;
#6466=CARTESIAN_POINT ( 'NONE',  ( 50.79490495164537833, 29.99999999999999645, -82.50000000000000000 ) ) ;
#6468=LINE ( 'NONE', #497, #4161 ) ;
#6472=ORIENTED_EDGE ( 'NONE', *, *, #2807, .T. ) ;
#6478=AXIS2_PLACEMENT_3D ( 'NONE', #2278, #2428, #5359 ) ;
#6481=DIRECTION ( 'NONE',  ( -0.5773502691896235106, -0.000000000000000000, 0.8164965809277276998 ) ) ;
#6483=EDGE_CURVE ( 'NONE', #458, #1974, #3806, .T. ) ;
#6484=ORIENTED_EDGE ( 'NONE', *, *, #6128, .F. ) ;
#6489=CIRCLE ( 'NONE', #7865, 11.00000000000000000 ) ;
#6490=DIRECTION ( 'NONE',  ( 0.000000000000000000, 0.000000000000000000, 1.000000000000000000 ) ) ;
#6496=ORIENTED_EDGE ( 'NONE', *, *, #6128, .T. ) ;
#6504=ORIENTED_EDGE ( 'NONE', *, *, #4714, .T. ) ;
#6506=CARTESIAN_POINT ( 'NONE',  ( 16.00000000000000000, 43.00000000000000000, -7.366666666666667140 ) ) ;
#6509=CARTESIAN_POINT ( 'NONE',  ( -50.79490495164537833, -12.50000000000000000, -100.0000000000000000 ) ) ;
#6513=VERTEX_POINT ( 'NONE', #2589 ) ;
#6518=CARTESIAN_POINT ( 'NONE',  ( 60.00000000000000000, 15.90990257669733943, -51.09009742330271564 ) ) ;
#6519=LINE ( 'NONE', #7276, #7149 ) ;
#6526=ORIENTED_EDGE ( 'NONE', *, *, #1111, .F. ) ;
#6527=DIRECTION ( 'NONE',  ( 0.000000000000000000, 0.000000000000000000, -1.000000000000000000 ) ) ;
#6528=AXIS2_PLACEMENT_3D ( 'NONE', #3386, #409, #1175 ) ;
#6532=CARTESIAN_POINT ( 'NONE',  ( 37.99999999999999289, -44.39318849903271769, -6.762951650419152472 ) ) ;
#6533=ADVANCED_FACE ( 'NONE', ( #2089 ), #7135, .T. ) ;
#6534=EDGE_CURVE ( 'NONE', #1974, #3407, #653, .T. ) ;
#6538=VERTEX_POINT ( 'NONE', #7904 ) ;
#6543=CIRCLE ( 'NONE', #7143, 3.000000000000002665 ) ;
#6546=CARTESIAN_POINT ( 'NONE',  ( -15.99999999999999645, 49.08300322764473123, -4.730698601353950039 ) ) ;
#6547=EDGE_CURVE ( 'NONE', #3622, #2677, #555, .T. ) ;
#6551=ORIENTED_EDGE ( 'NONE', *, *, #2603, .F. ) ;
#6554=DIRECTION ( 'NONE',  ( -0.000000000000000000, -0.000000000000000000, -1.000000000000000000 ) ) ;
#6558=DIRECTION ( 'NONE',  ( 0.5773502691896291728, -0.000000000000000000, 0.8164965809277235920 ) ) ;
#6564=ORIENTED_EDGE ( 'NONE', *, *, #6220, .F. ) ;
#6567=EDGE_LOOP ( 'NONE', ( #7193, #9214, #845, #2084 ) ) ;
#6579=STYLED_ITEM('',(#9515),#6348);
#6580=FACE_OUTER_BOUND ( 'NONE', #2149, .T. ) ;
#6581=CARTESIAN_POINT ( 'NONE',  ( -27.00000000000000000, 43.00000000000000000, 11.99999999999999645 ) ) ;
#6584=CARTESIAN_POINT ( 'NONE',  ( 37.22467645238197775, -47.05659850664388699, -5.608807313787648852 ) ) ;
#6585=APPLICATION_CONTEXT ( 'automotive_design' ) ;
#6594=CARTESIAN_POINT ( 'NONE',  ( -15.99999999999999645, 43.00000000000000000, -7.366666666666667140 ) ) ;
#6599=DIRECTION ( 'NONE',  ( 0.000000000000000000, 0.7071067811865479058, -0.7071067811865472397 ) ) ;
#6601=( BOUNDED_CURVE ( )  B_SPLINE_CURVE ( 3, ( #4570, #7546, #1635, #8355 ),
 .UNSPECIFIED., .F., .T. ) 
 B_SPLINE_CURVE_WITH_KNOTS ( ( 4, 4 ),
 ( 0.6692669939101993926, 1.047197551196597853 ),
 .UNSPECIFIED. ) 
 CURVE ( )  GEOMETRIC_REPRESENTATION_ITEM ( )  RATIONAL_B_SPLINE_CURVE ( ( 1.000000000000000000, 0.9881327504826167285, 0.9881327504826167285, 1.000000000000000000 ) ) 
 REPRESENTATION_ITEM ( '' )  );
#6602=EDGE_CURVE ( 'NONE', #6513, #1435, #893, .T. ) ;
#6613=VERTEX_POINT ( 'NONE', #507 ) ;
#6620=CARTESIAN_POINT ( 'NONE',  ( 37.00000000000000000, -15.90990257669733943, -85.90990257669729147 ) ) ;
#6637=DIRECTION ( 'NONE',  ( -1.000000000000000000, 0.000000000000000000, 0.000000000000000000 ) ) ;
#6641=CIRCLE ( 'NONE', #5870, 7.250000000000002665 ) ;
#6645=CARTESIAN_POINT ( 'NONE',  ( -15.99999999999999645, -43.00000000000000000, 11.99999999999999645 ) ) ;
#6646=ORIENTED_EDGE ( 'NONE', *, *, #6305, .F. ) ;
#6653=DIRECTION ( 'NONE',  ( 0.5773502691896271743, 0.000000000000000000, -0.8164965809277250353 ) ) ;
#6654=EDGE_CURVE ( 'NONE', #7697, #6367, #3974, .T. ) ;
#6656=VECTOR ( 'NONE', #4899, 999.9999999999998863 ) ;
#6660=DIRECTION ( 'NONE',  ( -1.000000000000000000, 0.000000000000000000, 0.000000000000000000 ) ) ;
#6663=DIRECTION ( 'NONE',  ( 1.000000000000000000, -0.000000000000000000, -0.000000000000000000 ) ) ;
#6664=CARTESIAN_POINT ( 'NONE',  ( -53.29490495164537833, -27.56180520566615044, -41.61356529332876875 ) ) ;
#6665=EDGE_CURVE ( 'NONE', #8519, #3283, #2277, .T. ) ;
#6668=ORIENTED_EDGE ( 'NONE', *, *, #5881, .T. ) ;
#6669=AXIS2_PLACEMENT_3D ( 'NONE', #290, #953, #6821 ) ;
#6671=EDGE_CURVE ( 'NONE', #3861, #3211, #6889, .T. ) ;
#6672=FACE_OUTER_BOUND ( 'NONE', #2783, .T. ) ;
#6678=ORIENTED_EDGE ( 'NONE', *, *, #9231, .F. ) ;
#6679=ORIENTED_EDGE ( 'NONE', *, *, #3410, .T. ) ;
#6691=ORIENTED_EDGE ( 'NONE', *, *, #6832, .F. ) ;
#6702=EDGE_LOOP ( 'NONE', ( #6133, #8376, #9456, #3655, #9044 ) ) ;
#6704=ADVANCED_FACE ( 'NONE', ( #2910 ), #2184, .F. ) ;
#6706=VECTOR ( 'NONE', #3667, 1000.000000000000000 ) ;
#6708=AXIS2_PLACEMENT_3D ( 'NONE', #6077, #8279, #6892 ) ;
#6720=AXIS2_PLACEMENT_3D ( 'NONE', #3371, #8652, #5588 ) ;
#6721=ORIENTED_EDGE ( 'NONE', *, *, #5159, .T. ) ;
#6722=VERTEX_POINT ( 'NONE', #3679 ) ;
#6726=CIRCLE ( 'NONE', #3032, 3.000000000000002665 ) ;
#6731=FACE_OUTER_BOUND ( 'NONE', #4065, .T. ) ;
#6738=DIRECTION ( 'NONE',  ( -0.000000000000000000, -0.000000000000000000, -1.000000000000000000 ) ) ;
#6745=DIRECTION ( 'NONE',  ( -1.000000000000000000, 0.000000000000000000, 0.000000000000000000 ) ) ;
#6746=FACE_OUTER_BOUND ( 'NONE', #946, .T. ) ;
#6747=AXIS2_PLACEMENT_3D ( 'NONE', #2933, #3753, #103 ) ;
#6751=LINE ( 'NONE', #3088, #2805 ) ;
#6754=EDGE_CURVE ( 'NONE', #301, #5309, #8102, .T. ) ;
#6757=ORIENTED_EDGE ( 'NONE', *, *, #3003, .T. ) ;
#6758=EDGE_CURVE ( 'NONE', #1561, #7674, #3725, .T. ) ;
#6760=CARTESIAN_POINT ( 'NONE',  ( 0.000000000000000000, 0.000000000000000000, 0.000000000000000000 ) ) ;
#6762=CARTESIAN_POINT ( 'NONE',  ( -51.96152422706632734, -30.00000000000000000, -80.85015119857382615 ) ) ;
#6765=DIRECTION ( 'NONE',  ( -1.000000000000000000, 0.000000000000000000, 0.000000000000000000 ) ) ;
#6766=CARTESIAN_POINT ( 'NONE',  ( 60.00000000000000000, 15.90990257669733943, -57.09009742330271564 ) ) ;
#6767=DIRECTION ( 'NONE',  ( 0.8660254037844399289, 0.000000000000000000, -0.4999999999999977240 ) ) ;
#6768=CARTESIAN_POINT ( 'NONE',  ( 39.50000000000000000, -14.99999999999999645, -97.50000000000001421 ) ) ;
#6771=EDGE_LOOP ( 'NONE', ( #3146, #8266, #4325, #7673 ) ) ;
#6774=ORIENTED_EDGE ( 'NONE', *, *, #4257, .T. ) ;
#6779=DIRECTION ( 'NONE',  ( 0.000000000000000000, 0.000000000000000000, 1.000000000000000000 ) ) ;
#6785=DIRECTION ( 'NONE',  ( 0.000000000000000000, 0.7071067811865473507, 0.7071067811865477948 ) ) ;
#6786=DIRECTION ( 'NONE',  ( 1.000000000000000000, 0.000000000000000000, 0.000000000000000000 ) ) ;
#6792=VECTOR ( 'NONE', #1061, 1000.000000000000000 ) ;
#6794=CARTESIAN_POINT ( 'NONE',  ( -37.00000000000000000, 30.00000000000000000, -13.00000000000000000 ) ) ;
#6797=CARTESIAN_POINT ( 'NONE',  ( 53.29490495164537833, 15.90990257669733943, -57.09009742330271564 ) ) ;
#6802=ORIENTED_EDGE ( 'NONE', *, *, #483, .T. ) ;
#6803=FACE_OUTER_BOUND ( 'NONE', #1481, .T. ) ;
#6804=CARTESIAN_POINT ( 'NONE',  ( -51.96152422706632734, -30.00000000000000000, -80.85015119857382615 ) ) ;
#6805=FACE_OUTER_BOUND ( 'NONE', #7719, .T. ) ;
#6807=AXIS2_PLACEMENT_3D ( 'NONE', #5581, #7100, #5680 ) ;
#6809=DIRECTION ( 'NONE',  ( -1.000000000000000000, 0.000000000000000000, 0.000000000000000000 ) ) ;
#6810=ORIENTED_EDGE ( 'NONE', *, *, #1848, .T. ) ;
#6812=FACE_OUTER_BOUND ( 'NONE', #8099, .T. ) ;
#6814=DIRECTION ( 'NONE',  ( 1.000000000000000000, -0.000000000000000000, 0.000000000000000000 ) ) ;
#6817=AXIS2_PLACEMENT_3D ( 'NONE', #899, #6908, #6809 ) ;
#6821=DIRECTION ( 'NONE',  ( 0.000000000000000000, 0.000000000000000000, 1.000000000000000000 ) ) ;
#6823=ORIENTED_EDGE ( 'NONE', *, *, #3307, .T. ) ;
#6829=DIRECTION ( 'NONE',  ( -1.000000000000000000, 0.000000000000000000, 0.000000000000000000 ) ) ;
#6832=EDGE_CURVE ( 'NONE', #4623, #5974, #8873, .T. ) ;
#6834=LINE ( 'NONE', #962, #3757 ) ;
#6840=VERTEX_POINT ( 'NONE', #1609 ) ;
#6852=DIRECTION ( 'NONE',  ( 1.000000000000000000, 0.000000000000000000, 0.000000000000000000 ) ) ;
#6853=LINE ( 'NONE', #7666, #8485 ) ;
#6857=DIRECTION ( 'NONE',  ( -0.4999999999999977240, 0.000000000000000000, -0.8660254037844399289 ) ) ;
#6861=ORIENTED_EDGE ( 'NONE', *, *, #3809, .F. ) ;
#6864=ORIENTED_EDGE ( 'NONE', *, *, #4777, .F. ) ;
#6868=VERTEX_POINT ( 'NONE', #222 ) ;
#6869=CARTESIAN_POINT ( 'NONE',  ( -9.364477336218600456, -62.15368297487813010, 0.9332626224471969323 ) ) ;
#6872=CARTESIAN_POINT ( 'NONE',  ( 37.00000000000000000, 15.90990257669733943, -85.90990257669729147 ) ) ;
#6876=EDGE_LOOP ( 'NONE', ( #5160, #7584, #8404, #9377 ) ) ;
#6877=AXIS2_PLACEMENT_3D ( 'NONE', #6396, #4804, #5681 ) ;
#6882=PLANE ( 'NONE',  #7639 ) ;
#6889=CIRCLE ( 'NONE', #5664, 11.00000000000000000 ) ;
#6891=DIRECTION ( 'NONE',  ( 1.000000000000000000, 0.000000000000000000, 0.000000000000000000 ) ) ;
#6892=DIRECTION ( 'NONE',  ( 0.000000000000000000, 0.000000000000000000, -1.000000000000000000 ) ) ;
#6900=EDGE_LOOP ( 'NONE', ( #2587, #8546, #870, #8894 ) ) ;
#6908=DIRECTION ( 'NONE',  ( -0.000000000000000000, -0.000000000000000000, -1.000000000000000000 ) ) ;
#6915=VERTEX_POINT ( 'NONE', #5506 ) ;
#6916=FACE_OUTER_BOUND ( 'NONE', #9146, .T. ) ;
#6919=ORIENTED_EDGE ( 'NONE', *, *, #9345, .F. ) ;
#6923=DIRECTION ( 'NONE',  ( 0.000000000000000000, -0.7071067811865479058, 0.7071067811865472397 ) ) ;
#6924=EDGE_CURVE ( 'NONE', #1076, #6279, #2439, .T. ) ;
#6926=EDGE_CURVE ( 'NONE', #5995, #1738, #6942, .T. ) ;
#6929=CARTESIAN_POINT ( 'NONE',  ( -34.25000000000000000, 43.00000000000000000, -25.00000000000000000 ) ) ;
#6931=DIRECTION ( 'NONE',  ( 0.000000000000000000, 0.7071067811865473507, 0.7071067811865477948 ) ) ;
#6932=VERTEX_POINT ( 'NONE', #8287 ) ;
#6933=LINE ( 'NONE', #2473, #48 ) ;
#6934=DIRECTION ( 'NONE',  ( 0.000000000000000000, 0.000000000000000000, 1.000000000000000000 ) ) ;
#6942=LINE ( 'NONE', #4593, #3114 ) ;
#6945=EDGE_CURVE ( 'NONE', #4995, #5110, #2353, .T. ) ;
#6948=DIRECTION ( 'NONE',  ( 0.000000000000000000, 0.000000000000000000, 1.000000000000000000 ) ) ;
#6953=ORIENTED_EDGE ( 'NONE', *, *, #8815, .F. ) ;
#6956=EDGE_LOOP ( 'NONE', ( #1783, #9163, #7560, #7824, #3863 ) ) ;
#6957=DIRECTION ( 'NONE',  ( 0.000000000000000000, 0.000000000000000000, -1.000000000000000000 ) ) ;
#6961=EDGE_CURVE ( 'NONE', #4881, #8783, #6853, .T. ) ;
#6965=DIRECTION ( 'NONE',  ( 0.000000000000000000, 0.000000000000000000, 1.000000000000000000 ) ) ;
#6967=ADVANCED_FACE ( 'NONE', ( #2526 ), #4782, .F. ) ;
#6969=ORIENTED_EDGE ( 'NONE', *, *, #6004, .F. ) ;
#6974=LINE ( 'NONE', #8271, #6792 ) ;
#6975=DIRECTION ( 'NONE',  ( -1.000000000000000000, 0.000000000000000000, 0.000000000000000000 ) ) ;
#6977=ORIENTED_EDGE ( 'NONE', *, *, #6924, .T. ) ;
#6978=CIRCLE ( 'NONE', #2207, 3.000000000000002665 ) ;
#6987=ORIENTED_EDGE ( 'NONE', *, *, #1536, .F. ) ;
#6991=DIRECTION ( 'NONE',  ( -1.000000000000000000, 0.000000000000000000, -0.000000000000000000 ) ) ;
#6992=CARTESIAN_POINT ( 'NONE',  ( 34.25000000000000000, 43.00000000000000000, 11.99999999999999645 ) ) ;
#7000=LINE ( 'NONE', #7769, #5360 ) ;
#7005=AXIS2_PLACEMENT_3D ( 'NONE', #7393, #1391, #2069 ) ;
#7008=FACE_OUTER_BOUND ( 'NONE', #7661, .T. ) ;
#7009=CIRCLE ( 'NONE', #8994, 3.000000000000002665 ) ;
#7010=ORIENTED_EDGE ( 'NONE', *, *, #9343, .T. ) ;
#7017=CARTESIAN_POINT ( 'NONE',  ( -27.00000000000000000, 43.00000000000000000, 11.99999999999999645 ) ) ;
#7020=EDGE_CURVE ( 'NONE', #7294, #1809, #3423, .T. ) ;
#7021=PLANE ( 'NONE',  #8183 ) ;
#7025=ORIENTED_EDGE ( 'NONE', *, *, #7654, .F. ) ;
#7031=CARTESIAN_POINT ( 'NONE',  ( -40.00000000000000000, -30.00000000000000000, -13.00000000000000533 ) ) ;
#7032=AXIS2_PLACEMENT_3D ( 'NONE', #6294, #9065, #3986 ) ;
#7033=ORIENTED_EDGE ( 'NONE', *, *, #9339, .F. ) ;
#7038=DIRECTION ( 'NONE',  ( 0.7071067811865475727, -0.000000000000000000, 0.7071067811865475727 ) ) ;
#7040=ADVANCED_FACE ( 'NONE', ( #8480 ), #7756, .F. ) ;
#7041=AXIS2_PLACEMENT_3D ( 'NONE', #5987, #3678, #6660 ) ;
#7050=ORIENTED_EDGE ( 'NONE', *, *, #435, .F. ) ;
#7051=DIRECTION ( 'NONE',  ( 0.000000000000000000, 1.000000000000000000, 0.000000000000000000 ) ) ;
#7062=DIRECTION ( 'NONE',  ( 0.000000000000000000, 0.000000000000000000, -1.000000000000000000 ) ) ;
#7063=PLANE ( 'NONE',  #6807 ) ;
#7064=FACE_OUTER_BOUND ( 'NONE', #6567, .T. ) ;
#7066=ORIENTED_EDGE ( 'NONE', *, *, #9254, .T. ) ;
#7075=EDGE_LOOP ( 'NONE', ( #6757, #6472 ) ) ;
#7078=ORIENTED_EDGE ( 'NONE', *, *, #913, .F. ) ;
#7083=VECTOR ( 'NONE', #6177, 999.9999999999998863 ) ;
#7088=ORIENTED_EDGE ( 'NONE', *, *, #6832, .T. ) ;
#7090=DIRECTION ( 'NONE',  ( -1.000000000000000000, 0.000000000000000000, 0.000000000000000000 ) ) ;
#7097=ORIENTED_EDGE ( 'NONE', *, *, #2624, .F. ) ;
#7099=DIRECTION ( 'NONE',  ( -1.000000000000000000, -0.000000000000000000, -0.000000000000000000 ) ) ;
#7100=DIRECTION ( 'NONE',  ( 0.000000000000000000, 0.000000000000000000, -1.000000000000000000 ) ) ;
#7101=CARTESIAN_POINT ( 'NONE',  ( -52.42476942962457542, 29.19763577280653877, -80.99738777760514097 ) ) ;
#7102=ORIENTED_EDGE ( 'NONE', *, *, #137, .T. ) ;
#7106=ORIENTED_EDGE ( 'NONE', *, *, #5881, .F. ) ;
#7112=DIRECTION ( 'NONE',  ( 1.000000000000000000, -0.000000000000000000, -0.000000000000000000 ) ) ;
#7114=VECTOR ( 'NONE', #4844, 1000.000000000000000 ) ;
#7123=AXIS2_PLACEMENT_3D ( 'NONE', #7234, #2235, #9443 ) ;
#7125=LINE ( 'NONE', #1943, #3387 ) ;
#7127=LINE ( 'NONE', #9335, #2530 ) ;
#7132=FACE_OUTER_BOUND ( 'NONE', #6453, .T. ) ;
#7133=ORIENTED_EDGE ( 'NONE', *, *, #9070, .F. ) ;
#7135=PLANE ( 'NONE',  #582 ) ;
#7137=CARTESIAN_POINT ( 'NONE',  ( 16.00000000000000000, -43.00000000000000000, 11.99999999999999645 ) ) ;
#7143=AXIS2_PLACEMENT_3D ( 'NONE', #8886, #5239, #5074 ) ;
#7144=DIRECTION ( 'NONE',  ( -0.000000000000000000, -0.000000000000000000, 1.000000000000000000 ) ) ;
#7149=VECTOR ( 'NONE', #9292, 1000.000000000000114 ) ;
#7154=ORIENTED_EDGE ( 'NONE', *, *, #4051, .T. ) ;
#7155=ORIENTED_EDGE ( 'NONE', *, *, #8116, .F. ) ;
#7160=DIRECTION ( 'NONE',  ( 1.000000000000000000, 0.000000000000000000, 0.000000000000000000 ) ) ;
#7164=VECTOR ( 'NONE', #6923, 999.9999999999998863 ) ;
#7166=AXIS2_PLACEMENT_3D ( 'NONE', #4986, #7336, #4218 ) ;
#7175=VECTOR ( 'NONE', #5029, 1000.000000000000000 ) ;
#7178=ORIENTED_EDGE ( 'NONE', *, *, #4842, .F. ) ;
#7181=ORIENTED_EDGE ( 'NONE', *, *, #6534, .F. ) ;
#7185=AXIS2_PLACEMENT_3D ( 'NONE', #8381, #1704, #6852 ) ;
#7188=DIRECTION ( 'NONE',  ( 0.000000000000000000, 0.000000000000000000, 1.000000000000000000 ) ) ;
#7192=AXIS2_PLACEMENT_3D ( 'NONE', #260, #8280, #3187 ) ;
#7193=ORIENTED_EDGE ( 'NONE', *, *, #805, .F. ) ;
#7199=CARTESIAN_POINT ( 'NONE',  ( 53.29490495164537833, -15.90990257669733943, -54.09009742330271564 ) ) ;
#7201=ORIENTED_EDGE ( 'NONE', *, *, #5424, .T. ) ;
#7204=( BOUNDED_CURVE ( )  B_SPLINE_CURVE ( 3, ( #2633, #4160, #3432, #603 ),
 .UNSPECIFIED., .F., .F. ) 
 B_SPLINE_CURVE_WITH_KNOTS ( ( 4, 4 ),
 ( 4.712388980384689674, 7.853981633974482790 ),
 .UNSPECIFIED. ) 
 CURVE ( )  GEOMETRIC_REPRESENTATION_ITEM ( )  RATIONAL_B_SPLINE_CURVE ( ( 1.000000000000000000, 0.3333333333333333703, 0.3333333333333333703, 1.000000000000000000 ) ) 
 REPRESENTATION_ITEM ( '' )  );
#7207=CARTESIAN_POINT ( 'NONE',  ( -15.99999999999999822, -20.99999999999999289, -16.89999999999999858 ) ) ;
#7209=DIRECTION ( 'NONE',  ( -1.000000000000000000, -0.000000000000000000, -0.000000000000000000 ) ) ;
#7212=ORIENTED_EDGE ( 'NONE', *, *, #6754, .T. ) ;
#7213=CARTESIAN_POINT ( 'NONE',  ( 27.00000000000000000, 43.00000000000000000, 11.99999999999999645 ) ) ;
#7216=EDGE_CURVE ( 'NONE', #8325, #7845, #3028, .T. ) ;
#7219=LINE ( 'NONE', #9429, #8432 ) ;
#7220=CARTESIAN_POINT ( 'NONE',  ( 37.00000000000000000, 13.96446609406729777, -95.00000000000000000 ) ) ;
#7221=LINE ( 'NONE', #8668, #4347 ) ;
#7223=EDGE_LOOP ( 'NONE', ( #5901, #2771, #8022, #577 ) ) ;
#7224=CARTESIAN_POINT ( 'NONE',  ( -38.00000000000000711, 43.00000000000000000, 11.99999999999999645 ) ) ;
#7225=ORIENTED_EDGE ( 'NONE', *, *, #7768, .T. ) ;
#7226=DIRECTION ( 'NONE',  ( 0.000000000000000000, 0.000000000000000000, 1.000000000000000000 ) ) ;
#7227=ADVANCED_FACE ( 'NONE', ( #5061, #2988 ), #5832, .T. ) ;
#7229=CARTESIAN_POINT ( 'NONE',  ( -12.55753963192698741, 30.00000000000000000, -8.879521428754452828 ) ) ;
#7231=EDGE_CURVE ( 'NONE', #8166, #6868, #5618, .T. ) ;
#7233=FACE_BOUND ( 'NONE', #1607, .T. ) ;
#7234=CARTESIAN_POINT ( 'NONE',  ( 0.000000000000000000, 0.000000000000000000, 25.00000000000000000 ) ) ;
#7248=ORIENTED_EDGE ( 'NONE', *, *, #4232, .T. ) ;
#7249=EDGE_LOOP ( 'NONE', ( #2951, #699 ) ) ;
#7250=AXIS2_PLACEMENT_3D ( 'NONE', #936, #356, #3240 ) ;
#7254=LINE ( 'NONE', #8836, #8100 ) ;
#7256=AXIS2_PLACEMENT_3D ( 'NONE', #1591, #1312, #5836 ) ;
#7261=CARTESIAN_POINT ( 'NONE',  ( 60.00000000000000000, -15.90990257669733943, -57.09009742330271564 ) ) ;
#7262=ORIENTED_EDGE ( 'NONE', *, *, #2823, .T. ) ;
#7265=DIRECTION ( 'NONE',  ( -0.000000000000000000, -0.000000000000000000, -1.000000000000000000 ) ) ;
#7272=ORIENTED_EDGE ( 'NONE', *, *, #2836, .T. ) ;
#7273=CARTESIAN_POINT ( 'NONE',  ( -53.29490495164537833, 27.56180520566615044, -41.61356529332876875 ) ) ;
#7276=CARTESIAN_POINT ( 'NONE',  ( 32.83333333333333570, -21.66666666666668206, -90.83333333333332860 ) ) ;
#7280=CARTESIAN_POINT ( 'NONE',  ( -53.29490495164537833, -1.836970198721028011E-15, -85.00000000000000000 ) ) ;
#7281=EDGE_CURVE ( 'NONE', #2677, #1076, #6933, .T. ) ;
#7283=ORIENTED_EDGE ( 'NONE', *, *, #5299, .T. ) ;
#7293=ORIENTED_EDGE ( 'NONE', *, *, #4461, .F. ) ;
#7294=VERTEX_POINT ( 'NONE', #5446 ) ;
#7296=EDGE_CURVE ( 'NONE', #5309, #6840, #6751, .T. ) ;
#7297=ORIENTED_EDGE ( 'NONE', *, *, #21, .F. ) ;
#7298=CARTESIAN_POINT ( 'NONE',  ( -37.00000000000000711, -15.90990257669733943, -85.90990257669729147 ) ) ;
#7308=AXIS2_PLACEMENT_3D ( 'NONE', #1903, #2678, #9242 ) ;
#7309=CARTESIAN_POINT ( 'NONE',  ( 26.21170834203230982, 53.97171801779368394, -2.612255525622733554 ) ) ;
#7321=AXIS2_PLACEMENT_3D ( 'NONE', #8223, #8985, #1646 ) ;
#7326=DIRECTION ( 'NONE',  ( -1.000000000000000000, 0.000000000000000000, 0.000000000000000000 ) ) ;
#7328=ADVANCED_FACE ( 'NONE', ( #2375 ), #1018, .F. ) ;
#7335=FACE_OUTER_BOUND ( 'NONE', #7401, .T. ) ;
#7336=DIRECTION ( 'NONE',  ( 0.000000000000000000, 0.000000000000000000, -1.000000000000000000 ) ) ;
#7338=FACE_BOUND ( 'NONE', #4661, .T. ) ;
#7341=ORIENTED_EDGE ( 'NONE', *, *, #3471, .T. ) ;
#7343=VERTEX_POINT ( 'NONE', #4003 ) ;
#7344=EDGE_CURVE ( 'NONE', #4223, #2372, #8226, .T. ) ;
#7346=ORIENTED_EDGE ( 'NONE', *, *, #5814, .F. ) ;
#7348=ADVANCED_FACE ( 'NONE', ( #1739 ), #3857, .T. ) ;
#7351=EDGE_CURVE ( 'NONE', #7415, #4522, #6189, .T. ) ;
#7362=EDGE_CURVE ( 'NONE', #4533, #6722, #6641, .T. ) ;
#7363=PLANE ( 'NONE',  #748 ) ;
#7364=DIRECTION ( 'NONE',  ( -0.000000000000000000, -0.000000000000000000, 1.000000000000000000 ) ) ;
#7370=CARTESIAN_POINT ( 'NONE',  ( -60.00000000000000000, 0.000000000000000000, -30.00000000000000000 ) ) ;
#7373=CARTESIAN_POINT ( 'NONE',  ( 60.00000000000000000, 15.90990257669733943, -57.09009742330271564 ) ) ;
#7374=LINE ( 'NONE', #4493, #3690 ) ;
#7376=CARTESIAN_POINT ( 'NONE',  ( -47.45689247961085044, -13.88265003728722924, -103.3380124720345350 ) ) ;
#7386=EDGE_CURVE ( 'NONE', #6538, #7697, #6489, .T. ) ;
#7387=FACE_BOUND ( 'NONE', #9072, .T. ) ;
#7389=CARTESIAN_POINT ( 'NONE',  ( -9.364477336218591574, 62.15368297487812299, 0.9332626224471912701 ) ) ;
#7392=EDGE_LOOP ( 'NONE', ( #6484, #335, #5298, #5425, #766, #4000, #7889, #7033, #5355, #8620, #5455, #6197 ) ) ;
#7393=CARTESIAN_POINT ( 'NONE',  ( -53.29490495164537833, -15.90990257669733943, -54.09009742330271564 ) ) ;
#7396=CYLINDRICAL_SURFACE ( 'NONE', #5719, 3.000000000000002665 ) ;
#7401=EDGE_LOOP ( 'NONE', ( #7955, #1411, #3577, #46 ) ) ;
#7404=EDGE_CURVE ( 'NONE', #2905, #975, #2655, .T. ) ;
#7406=CARTESIAN_POINT ( 'NONE',  ( 38.00000000000000000, -21.00000000000000000, -16.89999999999999858 ) ) ;
#7410=VECTOR ( 'NONE', #7531, 1000.000000000000000 ) ;
#7411=LINE ( 'NONE', #71, #2018 ) ;
#7414=CIRCLE ( 'NONE', #4963, 3.000000000000002665 ) ;
#7415=VERTEX_POINT ( 'NONE', #4905 ) ;
#7416=ORIENTED_EDGE ( 'NONE', *, *, #2533, .T. ) ;
#7417=DIRECTION ( 'NONE',  ( -1.000000000000000000, 0.000000000000000000, 0.000000000000000000 ) ) ;
#7419=CARTESIAN_POINT ( 'NONE',  ( 27.00000000000000000, -43.00000000000000000, 11.99999999999999645 ) ) ;
#7421=CARTESIAN_POINT ( 'NONE',  ( 16.00000000000000000, -43.00000000000000000, 11.99999999999999645 ) ) ;
#7428=DIRECTION ( 'NONE',  ( 1.000000000000000000, 0.000000000000000000, 0.000000000000000000 ) ) ;
#7432=CARTESIAN_POINT ( 'NONE',  ( -37.00000000000000000, -8.017766952966344007, -116.9822330470336453 ) ) ;
#7439=EDGE_CURVE ( 'NONE', #7294, #5417, #7555, .T. ) ;
#7442=DIRECTION ( 'NONE',  ( -1.000000000000000000, 0.000000000000000000, -0.000000000000000000 ) ) ;
#7447=CARTESIAN_POINT ( 'NONE',  ( 51.96152422706634155, -29.99999999999996447, -13.00000000000001066 ) ) ;
#7454=DIRECTION ( 'NONE',  ( 0.6785983445458479979, 0.2810846377148130126, -0.6785983445458491081 ) ) ;
#7460=ORIENTED_EDGE ( 'NONE', *, *, #6754, .F. ) ;
#7463=DIRECTION ( 'NONE',  ( -1.000000000000000000, 0.000000000000000000, 0.000000000000000000 ) ) ;
#7467=LINE ( 'NONE', #2911, #6394 ) ;
#7470=AXIS2_PLACEMENT_3D ( 'NONE', #3663, #4474, #3036 ) ;
#7472=DIRECTION ( 'NONE',  ( 0.000000000000000000, -0.7071067811865473507, -0.7071067811865477948 ) ) ;
#7473=VECTOR ( 'NONE', #8367, 1000.000000000000000 ) ;
#7475=AXIS2_PLACEMENT_3D ( 'NONE', #5142, #8129, #8024 ) ;
#7476=EDGE_LOOP ( 'NONE', ( #9, #6977, #3937, #6023, #9089, #4652 ) ) ;
#7485=CARTESIAN_POINT ( 'NONE',  ( -27.00000000000000000, 43.00000000000000000, 25.00000000000000000 ) ) ;
#7492=CIRCLE ( 'NONE', #7041, 7.250000000000002665 ) ;
#7493=CARTESIAN_POINT ( 'NONE',  ( 53.29490495164537833, 15.90990257669733943, -85.90990257669729147 ) ) ;
#7500=DIRECTION ( 'NONE',  ( -1.000000000000000000, 0.000000000000000000, 0.000000000000000000 ) ) ;
#7502=CIRCLE ( 'NONE', #2132, 3.000000000000002665 ) ;
#7512=VERTEX_POINT ( 'NONE', #9265 ) ;
#7513=SHAPE_REPRESENTATION_RELATIONSHIP ( 'NONE' , 'NONE' ,  #7573, #7727 ) ;
#7518=( BOUNDED_CURVE ( )  B_SPLINE_CURVE ( 3, ( #1326, #3304, #9295, #4797 ),
 .UNSPECIFIED., .F., .T. ) 
 B_SPLINE_CURVE_WITH_KNOTS ( ( 4, 4 ),
 ( 1.570796326794896558, 1.948494305174372609 ),
 .UNSPECIFIED. ) 
 CURVE ( )  GEOMETRIC_REPRESENTATION_ITEM ( )  RATIONAL_B_SPLINE_CURVE ( ( 1.000000000000000000, 0.9881473088045071851, 0.9881473088045071851, 1.000000000000000000 ) ) 
 REPRESENTATION_ITEM ( '' )  );
#7519=CARTESIAN_POINT ( 'NONE',  ( -38.00000000000000711, -43.00000000000000000, 11.99999999999999645 ) ) ;
#7520=DIRECTION ( 'NONE',  ( 0.000000000000000000, 0.000000000000000000, 1.000000000000000000 ) ) ;
#7521=CARTESIAN_POINT ( 'NONE',  ( -37.22467645238199196, -47.05659850664387278, 11.99999999999999645 ) ) ;
#7524=VERTEX_POINT ( 'NONE', #527 ) ;
#7528=CIRCLE ( 'NONE', #5230, 7.250000000000002665 ) ;
#7530=EDGE_CURVE ( 'NONE', #5683, #5609, #3106, .T. ) ;
#7531=DIRECTION ( 'NONE',  ( 0.000000000000000000, 0.000000000000000000, 1.000000000000000000 ) ) ;
#7536=CARTESIAN_POINT ( 'NONE',  ( -37.00000000000000711, 15.90990257669733943, -54.09009742330271564 ) ) ;
#7538=DIRECTION ( 'NONE',  ( -1.000000000000000000, 0.000000000000000000, 0.000000000000000000 ) ) ;
#7546=CARTESIAN_POINT ( 'NONE',  ( -43.18827341296429267, -42.33902489539480030, -7.653089211995582453 ) ) ;
#7551=CARTESIAN_POINT ( 'NONE',  ( -37.00000000000000711, 15.90990257669733943, -85.90990257669729147 ) ) ;
#7555=CIRCLE ( 'NONE', #2036, 60.00000000000000000 ) ;
#7558=ORIENTED_EDGE ( 'NONE', *, *, #228, .F. ) ;
#7559=ORIENTED_EDGE ( 'NONE', *, *, #3413, .T. ) ;
#7560=ORIENTED_EDGE ( 'NONE', *, *, #6961, .F. ) ;
#7561=EDGE_LOOP ( 'NONE', ( #4036, #6679 ) ) ;
#7562=DIRECTION ( 'NONE',  ( 1.000000000000000000, -0.000000000000000000, -0.000000000000000000 ) ) ;
#7565=EDGE_CURVE ( 'NONE', #5946, #5859, #5190, .T. ) ;
#7566=CARTESIAN_POINT ( 'NONE',  ( 27.00000000000000000, 43.00000000000000000, 11.99999999999999645 ) ) ;
#7573=SHAPE_REPRESENTATION ( '3-Flange Yoke', ( #1614 ), #6101 ) ;
#7575=EDGE_LOOP ( 'NONE', ( #6774, #4878 ) ) ;
#7579=FACE_OUTER_BOUND ( 'NONE', #3237, .T. ) ;
#7582=FACE_BOUND ( 'NONE', #53, .T. ) ;
#7583=CYLINDRICAL_SURFACE ( 'NONE', #2102, 11.00000000000000000 ) ;
#7584=ORIENTED_EDGE ( 'NONE', *, *, #6234, .T. ) ;
#7585=VERTEX_POINT ( 'NONE', #6594 ) ;
#7589=EDGE_CURVE ( 'NONE', #8372, #5946, #1629, .T. ) ;
#7590=VECTOR ( 'NONE', #6393, 1000.000000000000000 ) ;
#7591=DIRECTION ( 'NONE',  ( 0.000000000000000000, 0.000000000000000000, -1.000000000000000000 ) ) ;
#7596=VERTEX_POINT ( 'NONE', #8696 ) ;
#7597=ORIENTED_EDGE ( 'NONE', *, *, #1517, .F. ) ;
#7598=DIRECTION ( 'NONE',  ( -0.000000000000000000, -0.000000000000000000, 1.000000000000000000 ) ) ;
#7604=ORIENTED_EDGE ( 'NONE', *, *, #368, .F. ) ;
#7615=EDGE_CURVE ( 'NONE', #5090, #3120, #7914, .T. ) ;
#7619=DIRECTION ( 'NONE',  ( 0.000000000000000000, 0.7071067811865479058, -0.7071067811865472397 ) ) ;
#7621=ADVANCED_FACE ( 'NONE', ( #2976 ), #4329, .F. ) ;
#7624=CARTESIAN_POINT ( 'NONE',  ( 60.00000000000000000, 15.90990257669733943, -54.09009742330271564 ) ) ;
#7629=AXIS2_PLACEMENT_3D ( 'NONE', #706, #5225, #2196 ) ;
#7633=EDGE_LOOP ( 'NONE', ( #8509, #9423, #7262, #6102 ) ) ;
#7639=AXIS2_PLACEMENT_3D ( 'NONE', #8269, #915, #3892 ) ;
#7643=CARTESIAN_POINT ( 'NONE',  ( -19.74999999999999645, 43.00000000000000000, 11.99999999999999645 ) ) ;
#7649=DIRECTION ( 'NONE',  ( -1.000000000000000000, 0.000000000000000000, 0.000000000000000000 ) ) ;
#7652=CIRCLE ( 'NONE', #2279, 15.00000000000000000 ) ;
#7654=EDGE_CURVE ( 'NONE', #2690, #5694, #9462, .T. ) ;
#7656=CARTESIAN_POINT ( 'NONE',  ( -37.00000000000000711, -15.90990257669733943, -51.09009742330271564 ) ) ;
#7657=CARTESIAN_POINT ( 'NONE',  ( 51.96152422706634155, -29.99999999999996447, -13.00000000000001066 ) ) ;
#7658=CIRCLE ( 'NONE', #8878, 11.00000000000000000 ) ;
#7661=EDGE_LOOP ( 'NONE', ( #4968, #7248, #4698, #6204, #944, #8553 ) ) ;
#7665=EDGE_CURVE ( 'NONE', #6124, #4363, #3774, .T. ) ;
#7666=CARTESIAN_POINT ( 'NONE',  ( 49.75937104571250558, -12.92893218813459910, -101.0355339059328657 ) ) ;
#7668=CARTESIAN_POINT ( 'NONE',  ( -39.50000000000000711, -30.00000000000000355, -82.50000000000001421 ) ) ;
#7670=LINE ( 'NONE', #9055, #937 ) ;
#7673=ORIENTED_EDGE ( 'NONE', *, *, #3608, .F. ) ;
#7674=VERTEX_POINT ( 'NONE', #6012 ) ;
#7680=ORIENTED_EDGE ( 'NONE', *, *, #731, .T. ) ;
#7684=CARTESIAN_POINT ( 'NONE',  ( 27.00000000000000000, -43.00000000000000000, 11.99999999999999645 ) ) ;
#7690=LINE ( 'NONE', #3995, #2105 ) ;
#7697=VERTEX_POINT ( 'NONE', #5289 ) ;
#7700=CARTESIAN_POINT ( 'NONE',  ( -37.00000000000000711, -3.673940397442057600E-15, -70.00000000000000000 ) ) ;
#7701=DIRECTION ( 'NONE',  ( -1.000000000000000000, 0.000000000000000000, 0.000000000000000000 ) ) ;
#7705=ADVANCED_FACE ( 'NONE', ( #2639 ), #5571, .F. ) ;
#7708=ORIENTED_EDGE ( 'NONE', *, *, #5228, .T. ) ;
#7714=LINE ( 'NONE', #5556, #710 ) ;
#7715=LINE ( 'NONE', #1080, #5077 ) ;
#7719=EDGE_LOOP ( 'NONE', ( #2447, #2696, #7212, #2431, #3575, #6504 ) ) ;
#7721=CARTESIAN_POINT ( 'NONE',  ( -37.00000000000000000, -21.98223304703364889, -86.98223304703364533 ) ) ;
#7723=ADVANCED_FACE ( 'NONE', ( #2312 ), #859, .F. ) ;
#7724=CARTESIAN_POINT ( 'NONE',  ( 53.29490495164537833, -30.00000000000000000, -41.61356529332876875 ) ) ;
#7727=ADVANCED_BREP_SHAPE_REPRESENTATION ( '', ( #6348, #1614 ), #6101 ) ;
#7733=VERTEX_POINT ( 'NONE', #8169 ) ;
#7734=ORIENTED_EDGE ( 'NONE', *, *, #2543, .T. ) ;
#7739=DIRECTION ( 'NONE',  ( -1.000000000000000000, 0.000000000000000000, 0.000000000000000000 ) ) ;
#7740=FACE_OUTER_BOUND ( 'NONE', #9019, .T. ) ;
#7747=CARTESIAN_POINT ( 'NONE',  ( -50.79490495164537833, -30.00000000000000000, -100.0000000000000000 ) ) ;
#7752=ORIENTED_EDGE ( 'NONE', *, *, #56, .F. ) ;
#7756=PLANE ( 'NONE',  #6344 ) ;
#7764=EDGE_CURVE ( 'NONE', #6538, #8325, #2361, .T. ) ;
#7766=CARTESIAN_POINT ( 'NONE',  ( -40.00000000000000000, 30.00000000000000000, -13.00000000000000533 ) ) ;
#7768=EDGE_CURVE ( 'NONE', #3765, #1975, #4513, .T. ) ;
#7769=CARTESIAN_POINT ( 'NONE',  ( 60.00000000000000000, -3.673940397442057600E-15, -55.00000000000000711 ) ) ;
#7771=ORIENTED_EDGE ( 'NONE', *, *, #3123, .F. ) ;
#7773=CARTESIAN_POINT ( 'NONE',  ( 9.364477336218621772, -62.15368297487813010, 0.9332626224471951559 ) ) ;
#7775=CARTESIAN_POINT ( 'NONE',  ( 37.00000000000000000, -30.00000000000000000, -95.00000000000000000 ) ) ;
#7783=VECTOR ( 'NONE', #1300, 1000.000000000000000 ) ;
#7790=AXIS2_PLACEMENT_3D ( 'NONE', #7493, #961, #6115 ) ;
#7791=ORIENTED_EDGE ( 'NONE', *, *, #5948, .T. ) ;
#7805=CIRCLE ( 'NONE', #7185, 7.250000000000002665 ) ;
#7811=ORIENTED_EDGE ( 'NONE', *, *, #325, .F. ) ;
#7812=ORIENTED_EDGE ( 'NONE', *, *, #7296, .F. ) ;
#7814=AXIS2_PLACEMENT_3D ( 'NONE', #4718, #6975, #207 ) ;
#7819=CARTESIAN_POINT ( 'NONE',  ( 27.00000000000000000, -43.00000000000000000, -25.00000000000000000 ) ) ;
#7821=LINE ( 'NONE', #6435, #1438 ) ;
#7822=DIRECTION ( 'NONE',  ( -0.7071067811865481278, 0.000000000000000000, -0.7071067811865470176 ) ) ;
#7823=EDGE_CURVE ( 'NONE', #367, #2399, #6543, .T. ) ;
#7824=ORIENTED_EDGE ( 'NONE', *, *, #4414, .F. ) ;
#7825=ORIENTED_EDGE ( 'NONE', *, *, #6665, .F. ) ;
#7829=LINE ( 'NONE', #1147, #7590 ) ;
#7831=DIRECTION ( 'NONE',  ( -1.000000000000000000, 0.000000000000000000, -0.000000000000000000 ) ) ;
#7834=ORIENTED_EDGE ( 'NONE', *, *, #6, .T. ) ;
#7839=CARTESIAN_POINT ( 'NONE',  ( 39.50000000000000000, -30.00000000000000355, -82.50000000000001421 ) ) ;
#7842=ADVANCED_FACE ( 'NONE', ( #9347 ), #5030, .F. ) ;
#7845=VERTEX_POINT ( 'NONE', #8676 ) ;
#7846=DIRECTION ( 'NONE',  ( -0.5773502691896235106, -0.000000000000000000, -0.8164965809277276998 ) ) ;
#7851=CARTESIAN_POINT ( 'NONE',  ( 37.00000000000000000, -3.673940397442057600E-15, -70.00000000000000000 ) ) ;
#7865=AXIS2_PLACEMENT_3D ( 'NONE', #1785, #1067, #257 ) ;
#7866=LINE ( 'NONE', #611, #7114 ) ;
#7868=ORIENTED_EDGE ( 'NONE', *, *, #7439, .F. ) ;
#7879=ORIENTED_EDGE ( 'NONE', *, *, #8122, .F. ) ;
#7883=CARTESIAN_POINT ( 'NONE',  ( 0.000000000000000000, 0.000000000000000000, 11.99999999999999645 ) ) ;
#7884=DIRECTION ( 'NONE',  ( 0.000000000000000000, -1.000000000000000000, 0.000000000000000000 ) ) ;
#7889=ORIENTED_EDGE ( 'NONE', *, *, #5015, .F. ) ;
#7894=LINE ( 'NONE', #8572, #8385 ) ;
#7895=DIRECTION ( 'NONE',  ( 1.000000000000000000, -0.000000000000000000, -0.000000000000000000 ) ) ;
#7896=AXIS2_PLACEMENT_3D ( 'NONE', #2553, #3849, #6118 ) ;
#7900=ORIENTED_EDGE ( 'NONE', *, *, #3897, .T. ) ;
#7904=CARTESIAN_POINT ( 'NONE',  ( 38.00000000000000000, 43.00000000000000000, 11.99999999999999645 ) ) ;
#7914=CIRCLE ( 'NONE', #7005, 3.000000000000002665 ) ;
#7916=ADVANCED_FACE ( 'NONE', ( #5757 ), #2865, .F. ) ;
#7919=AXIS2_PLACEMENT_3D ( 'NONE', #3727, #1514, #4595 ) ;
#7920=LINE ( 'NONE', #2747, #2359 ) ;
#7922=VERTEX_POINT ( 'NONE', #3533 ) ;
#7925=ORIENTED_EDGE ( 'NONE', *, *, #3548, .T. ) ;
#7926=ORIENTED_EDGE ( 'NONE', *, *, #4842, .T. ) ;
#7935=ADVANCED_FACE ( 'NONE', ( #6383 ), #1269, .F. ) ;
#7937=( BOUNDED_CURVE ( )  B_SPLINE_CURVE ( 3, ( #4465, #7389, #4420, #5085 ),
 .UNSPECIFIED., .F., .F. ) 
 B_SPLINE_CURVE_WITH_KNOTS ( ( 4, 4 ),
 ( 5.831078311124174185, 6.735292303234999167 ),
 .UNSPECIFIED. ) 
 CURVE ( )  GEOMETRIC_REPRESENTATION_ITEM ( )  RATIONAL_B_SPLINE_CURVE ( ( 1.000000000000000000, 0.9330190890865965869, 0.9330190890865965869, 1.000000000000000000 ) ) 
 REPRESENTATION_ITEM ( '' )  );
#7939=ORIENTED_EDGE ( 'NONE', *, *, #5243, .T. ) ;
#7940=EDGE_CURVE ( 'NONE', #580, #900, #5708, .T. ) ;
#7942=EDGE_CURVE ( 'NONE', #7512, #3144, #6519, .T. ) ;
#7955=ORIENTED_EDGE ( 'NONE', *, *, #4124, .F. ) ;
#7956=CARTESIAN_POINT ( 'NONE',  ( 37.00000000000000000, -21.98223304703365244, -86.98223304703364533 ) ) ;
#7958=EDGE_CURVE ( 'NONE', #8859, #490, #5891, .T. ) ;
#7962=CIRCLE ( 'NONE', #5808, 7.250000000000002665 ) ;
#7963=EDGE_CURVE ( 'NONE', #490, #3514, #951, .T. ) ;
#7966=FACE_BOUND ( 'NONE', #3675, .T. ) ;
#7979=ORIENTED_EDGE ( 'NONE', *, *, #251, .T. ) ;
#7993=EDGE_CURVE ( 'NONE', #5804, #5660, #8241, .T. ) ;
#7994=CARTESIAN_POINT ( 'NONE',  ( 37.00000000000000000, -1.836970198721028011E-15, -85.00000000000000000 ) ) ;
#7997=ORIENTED_EDGE ( 'NONE', *, *, #2810, .T. ) ;
#7999=CARTESIAN_POINT ( 'NONE',  ( -37.00000000000000711, -15.90990257669733943, -82.90990257669729147 ) ) ;
#8000=ORIENTED_EDGE ( 'NONE', *, *, #7530, .T. ) ;
#8005=CARTESIAN_POINT ( 'NONE',  ( 37.00000000000000000, 15.90990257669733943, -51.09009742330271564 ) ) ;
#8009=ORIENTED_EDGE ( 'NONE', *, *, #7940, .T. ) ;
#8015=CARTESIAN_POINT ( 'NONE',  ( 38.00000000000000000, -43.00000000000000000, -7.366666666666667140 ) ) ;
#8016=CARTESIAN_POINT ( 'NONE',  ( -60.00000000000000000, 0.000000000000000000, -30.00000000000000000 ) ) ;
#8017=ORIENTED_EDGE ( 'NONE', *, *, #9339, .T. ) ;
#8020=ORIENTED_EDGE ( 'NONE', *, *, #3608, .T. ) ;
#8022=ORIENTED_EDGE ( 'NONE', *, *, #8055, .F. ) ;
#8024=DIRECTION ( 'NONE',  ( 0.000000000000000000, 0.000000000000000000, 1.000000000000000000 ) ) ;
#8029=ADVANCED_FACE ( 'NONE', ( #3000, #5845 ), #3100, .T. ) ;
#8032=DIRECTION ( 'NONE',  ( 0.000000000000000000, -0.7071067811865479058, 0.7071067811865472397 ) ) ;
#8033=ORIENTED_EDGE ( 'NONE', *, *, #331, .F. ) ;
#8037=DIRECTION ( 'NONE',  ( 0.000000000000000000, 0.9175556253099241832, -0.3976074376343005090 ) ) ;
#8042=( LENGTH_UNIT ( ) NAMED_UNIT ( * ) SI_UNIT ( .MILLI., .METRE. ) );
#8046=CARTESIAN_POINT ( 'NONE',  ( 60.00000000000000000, -3.673940397442057600E-15, -55.00000000000000711 ) ) ;
#8047=CARTESIAN_POINT ( 'NONE',  ( 60.00000000000001421, 9.637301612213116542, -29.99999999999998934 ) ) ;
#8052=EDGE_CURVE ( 'NONE', #6279, #8200, #7467, .T. ) ;
#8055=EDGE_CURVE ( 'NONE', #287, #8464, #7009, .T. ) ;
#8056=EDGE_LOOP ( 'NONE', ( #6050, #2253, #172, #2840 ) ) ;
#8065=ADVANCED_FACE ( 'NONE', ( #8770 ), #2400, .T. ) ;
#8075=CARTESIAN_POINT ( 'NONE',  ( 52.86930915046634283, 28.38475884032109775, -81.18159060786257442 ) ) ;
#8077=DIRECTION ( 'NONE',  ( 0.000000000000000000, 0.000000000000000000, -1.000000000000000000 ) ) ;
#8081=LINE ( 'NONE', #3707, #2099 ) ;
#8094=ORIENTED_EDGE ( 'NONE', *, *, #1049, .F. ) ;
#8096=ORIENTED_EDGE ( 'NONE', *, *, #4139, .F. ) ;
#8098=CIRCLE ( 'NONE', #3960, 3.000000000000002665 ) ;
#8099=EDGE_LOOP ( 'NONE', ( #9195, #4016, #7812 ) ) ;
#8100=VECTOR ( 'NONE', #1488, 1000.000000000000000 ) ;
#8101=CARTESIAN_POINT ( 'NONE',  ( -53.29490495164537833, 27.56180520566615044, -134.0000000000000284 ) ) ;
#8102=LINE ( 'NONE', #5164, #4427 ) ;
#8103=LINE ( 'NONE', #7519, #9141 ) ;
#8106=FACE_OUTER_BOUND ( 'NONE', #4589, .T. ) ;
#8114=ORIENTED_EDGE ( 'NONE', *, *, #4139, .T. ) ;
#8116=EDGE_CURVE ( 'NONE', #7524, #6045, #5928, .T. ) ;
#8120=FACE_BOUND ( 'NONE', #2749, .T. ) ;
#8121=EDGE_CURVE ( 'NONE', #550, #5932, #8103, .T. ) ;
#8122=EDGE_CURVE ( 'NONE', #8200, #523, #7714, .T. ) ;
#8127=VERTEX_POINT ( 'NONE', #2486 ) ;
#8129=DIRECTION ( 'NONE',  ( 1.000000000000000000, -0.000000000000000000, -0.000000000000000000 ) ) ;
#8132=DIRECTION ( 'NONE',  ( 1.000000000000000000, -0.000000000000000000, -0.000000000000000000 ) ) ;
#8135=EDGE_LOOP ( 'NONE', ( #8554, #1927, #8607, #3827 ) ) ;
#8146=( NAMED_UNIT ( * ) SI_UNIT ( $, .STERADIAN. ) SOLID_ANGLE_UNIT ( ) );
#8147=VERTEX_POINT ( 'NONE', #5458 ) ;
#8148=LINE ( 'NONE', #8101, #2286 ) ;
#8151=CARTESIAN_POINT ( 'NONE',  ( 53.29490495164537833, 27.56180520566613268, -41.61356529332876875 ) ) ;
#8152=DIRECTION ( 'NONE',  ( 0.000000000000000000, 0.000000000000000000, -1.000000000000000000 ) ) ;
#8157=ORIENTED_EDGE ( 'NONE', *, *, #7942, .F. ) ;
#8158=DIRECTION ( 'NONE',  ( -0.000000000000000000, -0.000000000000000000, 1.000000000000000000 ) ) ;
#8160=VECTOR ( 'NONE', #7364, 1000.000000000000000 ) ;
#8166=VERTEX_POINT ( 'NONE', #8383 ) ;
#8169=CARTESIAN_POINT ( 'NONE',  ( -53.29490495164537833, 15.90990257669733943, -82.90990257669729147 ) ) ;
#8173=PLANE ( 'NONE',  #8731 ) ;
#8175=ADVANCED_FACE ( 'NONE', ( #938 ), #4018, .T. ) ;
#8181=CARTESIAN_POINT ( 'NONE',  ( 38.00000000000000000, -43.00000000000000000, -7.366666666666667140 ) ) ;
#8183=AXIS2_PLACEMENT_3D ( 'NONE', #9125, #3366, #1691 ) ;
#8193=( BOUNDED_CURVE ( )  B_SPLINE_CURVE ( 3, ( #1816, #7773, #6869, #3932 ),
 .UNSPECIFIED., .F., .F. ) 
 B_SPLINE_CURVE_WITH_KNOTS ( ( 4, 4 ),
 ( 5.831078311124173297, 6.735292303234999167 ),
 .UNSPECIFIED. ) 
 CURVE ( )  GEOMETRIC_REPRESENTATION_ITEM ( )  RATIONAL_B_SPLINE_CURVE ( ( 1.000000000000000000, 0.9330190890865963649, 0.9330190890865963649, 1.000000000000000000 ) ) 
 REPRESENTATION_ITEM ( '' )  );
#8195=VECTOR ( 'NONE', #2458, 1000.000000000000000 ) ;
#8199=CARTESIAN_POINT ( 'NONE',  ( 37.22467645238198486, 47.05659850664387989, 11.99999999999999645 ) ) ;
#8200=VERTEX_POINT ( 'NONE', #7668 ) ;
#8201=AXIS2_PLACEMENT_3D ( 'NONE', #8263, #3989, #7538 ) ;
#8202=EDGE_LOOP ( 'NONE', ( #1950, #6721 ) ) ;
#8207=CARTESIAN_POINT ( 'NONE',  ( -37.00000000000000000, -30.00000000000000000, -78.96446609406729067 ) ) ;
#8211=ORIENTED_EDGE ( 'NONE', *, *, #8563, .F. ) ;
#8217=LINE ( 'NONE', #5095, #645 ) ;
#8220=CARTESIAN_POINT ( 'NONE',  ( -27.00000000000000000, 43.00000000000000000, 11.99999999999999645 ) ) ;
#8221=CARTESIAN_POINT ( 'NONE',  ( 60.00000000000000000, -3.673940397442057600E-15, -70.00000000000000000 ) ) ;
#8223=CARTESIAN_POINT ( 'NONE',  ( 27.00000000000000000, -43.00000000000000000, 11.99999999999999645 ) ) ;
#8225=AXIS2_PLACEMENT_3D ( 'NONE', #3169, #6738, #6062 ) ;
#8226=LINE ( 'NONE', #9129, #495 ) ;
#8229=EDGE_CURVE ( 'NONE', #8147, #3234, #1033, .T. ) ;
#8232=VECTOR ( 'NONE', #3925, 1000.000000000000000 ) ;
#8236=EDGE_LOOP ( 'NONE', ( #7088, #5287 ) ) ;
#8237=VERTEX_POINT ( 'NONE', #6804 ) ;
#8238=EDGE_LOOP ( 'NONE', ( #5137, #3503 ) ) ;
#8239=LINE ( 'NONE', #3969, #6130 ) ;
#8241=LINE ( 'NONE', #7373, #1017 ) ;
#8248=DIRECTION ( 'NONE',  ( 0.000000000000000000, 0.000000000000000000, -1.000000000000000000 ) ) ;
#8252=AXIS2_PLACEMENT_3D ( 'NONE', #4810, #3414, #5000 ) ;
#8258=VECTOR ( 'NONE', #4655, 999.9999999999998863 ) ;
#8260=ORIENTED_EDGE ( 'NONE', *, *, #5424, .F. ) ;
#8263=CARTESIAN_POINT ( 'NONE',  ( 27.00000000000000000, 43.00000000000000000, 11.99999999999999645 ) ) ;
#8266=ORIENTED_EDGE ( 'NONE', *, *, #6926, .F. ) ;
#8268=DIRECTION ( 'NONE',  ( 0.000000000000000000, 0.000000000000000000, 1.000000000000000000 ) ) ;
#8269=CARTESIAN_POINT ( 'NONE',  ( 0.000000000000000000, -30.00000000000000000, 0.000000000000000000 ) ) ;
#8271=CARTESIAN_POINT ( 'NONE',  ( 60.00000000000000000, 15.90990257669733943, -82.90990257669729147 ) ) ;
#8273=DIRECTION ( 'NONE',  ( -0.000000000000000000, -0.000000000000000000, 1.000000000000000000 ) ) ;
#8275=ORIENTED_EDGE ( 'NONE', *, *, #5948, .F. ) ;
#8277=VERTEX_POINT ( 'NONE', #3569 ) ;
#8278=DIRECTION ( 'NONE',  ( -0.000000000000000000, 1.000000000000000000, 0.000000000000000000 ) ) ;
#8279=DIRECTION ( 'NONE',  ( -1.000000000000000000, 0.000000000000000000, -0.000000000000000000 ) ) ;
#8280=DIRECTION ( 'NONE',  ( 0.000000000000000000, -0.7071067811865472397, -0.7071067811865479058 ) ) ;
#8283=ORIENTED_EDGE ( 'NONE', *, *, #4225, .T. ) ;
#8284=VERTEX_POINT ( 'NONE', #3425 ) ;
#8286=CARTESIAN_POINT ( 'NONE',  ( -52.42476942962461095, -29.19763577280653877, -80.99738777760511255 ) ) ;
#8287=CARTESIAN_POINT ( 'NONE',  ( -50.79490495164537833, 12.50000000000000000, -100.0000000000000000 ) ) ;
#8295=ORIENTED_EDGE ( 'NONE', *, *, #7231, .T. ) ;
#8296=DIRECTION ( 'NONE',  ( -0.000000000000000000, -0.000000000000000000, 1.000000000000000000 ) ) ;
#8298=ORIENTED_EDGE ( 'NONE', *, *, #3547, .T. ) ;
#8303=EDGE_CURVE ( 'NONE', #804, #3622, #7894, .T. ) ;
#8304=AXIS2_PLACEMENT_3D ( 'NONE', #7566, #317, #9096 ) ;
#8305=FACE_OUTER_BOUND ( 'NONE', #4350, .T. ) ;
#8307=ORIENTED_EDGE ( 'NONE', *, *, #7404, .F. ) ;
#8314=LINE ( 'NONE', #6929, #1427 ) ;
#8325=VERTEX_POINT ( 'NONE', #4242 ) ;
#8330=CYLINDRICAL_SURFACE ( 'NONE', #2551, 3.000000000000002665 ) ;
#8340=VERTEX_POINT ( 'NONE', #6466 ) ;
#8352=ORIENTED_EDGE ( 'NONE', *, *, #4232, .F. ) ;
#8355=CARTESIAN_POINT ( 'NONE',  ( -51.96152422706632024, -30.00000000000000000, -13.00000000000000000 ) ) ;
#8358=( BOUNDED_CURVE ( )  B_SPLINE_CURVE ( 3, ( #3710, #4381, #2852, #7309 ),
 .UNSPECIFIED., .F., .T. ) 
 B_SPLINE_CURVE_WITH_KNOTS ( ( 4, 4 ),
 ( 1.570796326794896558, 3.069868295139984049 ),
 .UNSPECIFIED. ) 
 CURVE ( )  GEOMETRIC_REPRESENTATION_ITEM ( )  RATIONAL_B_SPLINE_CURVE ( ( 1.000000000000000000, 0.8213367208436757050, 0.8213367208436757050, 1.000000000000000000 ) ) 
 REPRESENTATION_ITEM ( '' )  );
#8367=DIRECTION ( 'NONE',  ( 0.000000000000000000, 1.000000000000000000, 0.000000000000000000 ) ) ;
#8372=VERTEX_POINT ( 'NONE', #7999 ) ;
#8373=FACE_OUTER_BOUND ( 'NONE', #6702, .T. ) ;
#8375=ORIENTED_EDGE ( 'NONE', *, *, #9280, .T. ) ;
#8376=ORIENTED_EDGE ( 'NONE', *, *, #56, .T. ) ;
#8381=CARTESIAN_POINT ( 'NONE',  ( -27.00000000000000000, -43.00000000000000000, 25.00000000000000000 ) ) ;
#8383=CARTESIAN_POINT ( 'NONE',  ( 16.00000000000000000, -43.00000000000000000, -7.366666666666667140 ) ) ;
#8384=CARTESIAN_POINT ( 'NONE',  ( -41.99999999999999289, 12.50000000000000000, -100.0000000000000000 ) ) ;
#8385=VECTOR ( 'NONE', #2767, 1000.000000000000000 ) ;
#8386=CARTESIAN_POINT ( 'NONE',  ( -37.22467645238198486, 47.05659850664388699, -5.608807313787648852 ) ) ;
#8389=ORIENTED_EDGE ( 'NONE', *, *, #5371, .T. ) ;
#8394=CARTESIAN_POINT ( 'NONE',  ( 39.50000000000000000, 29.99999999999999645, -82.50000000000000000 ) ) ;
#8396=ORIENTED_EDGE ( 'NONE', *, *, #7020, .T. ) ;
#8397=CIRCLE ( 'NONE', #7470, 3.000000000000002665 ) ;
#8398=DIRECTION ( 'NONE',  ( 1.000000000000000000, 0.000000000000000000, 0.000000000000000000 ) ) ;
#8400=CIRCLE ( 'NONE', #568, 7.250000000000002665 ) ;
#8404=ORIENTED_EDGE ( 'NONE', *, *, #7386, .T. ) ;
#8407=SHAPE_DEFINITION_REPRESENTATION ( #4922, #7573 ) ;
#8411=EDGE_CURVE ( 'NONE', #2905, #75, #8799, .T. ) ;
#8412=AXIS2_PLACEMENT_3D ( 'NONE', #5438, #963, #8416 ) ;
#8416=DIRECTION ( 'NONE',  ( 0.000000000000000000, 0.000000000000000000, 1.000000000000000000 ) ) ;
#8418=DIRECTION ( 'NONE',  ( 1.000000000000000000, 0.000000000000000000, 0.000000000000000000 ) ) ;
#8420=CARTESIAN_POINT ( 'NONE',  ( -37.00000000000000711, 15.90990257669733943, -82.90990257669729147 ) ) ;
#8424=CIRCLE ( 'NONE', #1842, 3.000000000000002665 ) ;
#8431=EDGE_CURVE ( 'NONE', #6279, #2195, #3089, .T. ) ;
#8432=VECTOR ( 'NONE', #7454, 1000.000000000000114 ) ;
#8439=DIRECTION ( 'NONE',  ( 0.000000000000000000, -1.000000000000000000, 0.000000000000000000 ) ) ;
#8448=FACE_BOUND ( 'NONE', #1153, .T. ) ;
#8450=LINE ( 'NONE', #2640, #4769 ) ;
#8452=DIRECTION ( 'NONE',  ( -1.000000000000000000, 0.000000000000000000, 0.000000000000000000 ) ) ;
#8464=VERTEX_POINT ( 'NONE', #821 ) ;
#8469=FACE_OUTER_BOUND ( 'NONE', #1759, .T. ) ;
#8474=LINE ( 'NONE', #7031, #7783 ) ;
#8476=ORIENTED_EDGE ( 'NONE', *, *, #7823, .T. ) ;
#8477=ORIENTED_EDGE ( 'NONE', *, *, #6926, .T. ) ;
#8479=ORIENTED_EDGE ( 'NONE', *, *, #6483, .T. ) ;
#8480=FACE_OUTER_BOUND ( 'NONE', #2472, .T. ) ;
#8485=VECTOR ( 'NONE', #9093, 1000.000000000000114 ) ;
#8491=LINE ( 'NONE', #9290, #2123 ) ;
#8497=DIRECTION ( 'NONE',  ( -0.000000000000000000, -0.000000000000000000, -1.000000000000000000 ) ) ;
#8498=ORIENTED_EDGE ( 'NONE', *, *, #2452, .F. ) ;
#8502=DIRECTION ( 'NONE',  ( -1.000000000000000000, 0.000000000000000000, -0.000000000000000000 ) ) ;
#8503=CARTESIAN_POINT ( 'NONE',  ( 50.79490495164537833, 29.99999999999999645, -82.50000000000000000 ) ) ;
#8509=ORIENTED_EDGE ( 'NONE', *, *, #7993, .F. ) ;
#8515=DIRECTION ( 'NONE',  ( 0.000000000000000000, -0.000000000000000000, 1.000000000000000000 ) ) ;
#8518=VERTEX_POINT ( 'NONE', #6794 ) ;
#8519=VERTEX_POINT ( 'NONE', #3905 ) ;
#8520=EDGE_CURVE ( 'NONE', #804, #8237, #1508, .T. ) ;
#8535=ORIENTED_EDGE ( 'NONE', *, *, #5657, .T. ) ;
#8537=DIRECTION ( 'NONE',  ( 0.000000000000000000, 0.000000000000000000, -1.000000000000000000 ) ) ;
#8543=CARTESIAN_POINT ( 'NONE',  ( -39.50000000000000711, 15.00000000000000533, -97.50000000000001421 ) ) ;
#8544=EDGE_CURVE ( 'NONE', #472, #1561, #721, .T. ) ;
#8546=ORIENTED_EDGE ( 'NONE', *, *, #8052, .F. ) ;
#8550=CARTESIAN_POINT ( 'NONE',  ( -37.22467645238198486, 47.05659850664388699, -5.608807313787648852 ) ) ;
#8553=ORIENTED_EDGE ( 'NONE', *, *, #3547, .F. ) ;
#8554=ORIENTED_EDGE ( 'NONE', *, *, #3471, .F. ) ;
#8555=ORIENTED_EDGE ( 'NONE', *, *, #5772, .T. ) ;
#8557=ORIENTED_EDGE ( 'NONE', *, *, #5129, .T. ) ;
#8558=DIRECTION ( 'NONE',  ( 0.000000000000000000, 0.000000000000000000, -1.000000000000000000 ) ) ;
#8561=DIRECTION ( 'NONE',  ( 0.000000000000000000, 0.000000000000000000, -1.000000000000000000 ) ) ;
#8562=DIRECTION ( 'NONE',  ( 1.000000000000000000, -0.000000000000000000, -0.000000000000000000 ) ) ;
#8563=EDGE_CURVE ( 'NONE', #2915, #6915, #1327, .T. ) ;
#8569=ORIENTED_EDGE ( 'NONE', *, *, #5542, .F. ) ;
#8572=CARTESIAN_POINT ( 'NONE',  ( -60.00000000000000000, -30.00000000000000000, -13.00000000000000000 ) ) ;
#8574=CARTESIAN_POINT ( 'NONE',  ( 38.00000000000000000, 43.00000000000000000, -7.366666666666667140 ) ) ;
#8575=CIRCLE ( 'NONE', #4750, 15.00000000000000000 ) ;
#8599=CIRCLE ( 'NONE', #4463, 3.000000000000002665 ) ;
#8601=DIRECTION ( 'NONE',  ( 0.000000000000000000, 0.000000000000000000, -1.000000000000000000 ) ) ;
#8602=CYLINDRICAL_SURFACE ( 'NONE', #2877, 11.00000000000000711 ) ;
#8607=ORIENTED_EDGE ( 'NONE', *, *, #8116, .T. ) ;
#8608=EDGE_LOOP ( 'NONE', ( #8901, #1399, #7879, #857, #4558, #3713 ) ) ;
#8612=CARTESIAN_POINT ( 'NONE',  ( -26.21170834203230982, -53.97171801779368394, -0.5000000000000038858 ) ) ;
#8616=DIRECTION ( 'NONE',  ( 0.000000000000000000, 0.000000000000000000, 1.000000000000000000 ) ) ;
#8617=AXIS2_PLACEMENT_3D ( 'NONE', #727, #2267, #102 ) ;
#8619=DIRECTION ( 'NONE',  ( -0.000000000000000000, -0.000000000000000000, -1.000000000000000000 ) ) ;
#8620=ORIENTED_EDGE ( 'NONE', *, *, #5542, .T. ) ;
#8626=CARTESIAN_POINT ( 'NONE',  ( -27.00000000000000000, -43.00000000000000000, -25.00000000000000000 ) ) ;
#8632=ORIENTED_EDGE ( 'NONE', *, *, #633, .T. ) ;
#8637=EDGE_CURVE ( 'NONE', #900, #55, #4004, .T. ) ;
#8643=EDGE_CURVE ( 'NONE', #8518, #3622, #2660, .T. ) ;
#8644=DIRECTION ( 'NONE',  ( 0.000000000000000000, 0.000000000000000000, -1.000000000000000000 ) ) ;
#8649=ORIENTED_EDGE ( 'NONE', *, *, #9396, .F. ) ;
#8652=DIRECTION ( 'NONE',  ( 0.000000000000000000, 0.000000000000000000, -1.000000000000000000 ) ) ;
#8653=CARTESIAN_POINT ( 'NONE',  ( 0.000000000000000000, 0.000000000000000000, 23.99999999999998579 ) ) ;
#8654=ADVANCED_FACE ( 'NONE', ( #6455 ), #2613, .F. ) ;
#8658=EDGE_CURVE ( 'NONE', #5932, #2310, #4321, .T. ) ;
#8659=ORIENTED_EDGE ( 'NONE', *, *, #800, .F. ) ;
#8662=ORIENTED_EDGE ( 'NONE', *, *, #1004, .T. ) ;
#8665=DIRECTION ( 'NONE',  ( -1.000000000000000000, 0.000000000000000000, 0.000000000000000000 ) ) ;
#8668=CARTESIAN_POINT ( 'NONE',  ( 60.00000000000000000, 29.99999999999999645, -82.50000000000000000 ) ) ;
#8670=CIRCLE ( 'NONE', #9142, 3.000000000000002665 ) ;
#8676=CARTESIAN_POINT ( 'NONE',  ( 16.00000000000000000, 43.00000000000000000, -7.366666666666667140 ) ) ;
#8685=LINE ( 'NONE', #2104, #3030 ) ;
#8687=CIRCLE ( 'NONE', #6528, 7.250000000000002665 ) ;
#8690=VERTEX_POINT ( 'NONE', #4286 ) ;
#8696=CARTESIAN_POINT ( 'NONE',  ( 39.50000000000000000, 15.00000000000001066, -97.50000000000000000 ) ) ;
#8703=CARTESIAN_POINT ( 'NONE',  ( -26.21170834203229205, 53.97171801779368394, 11.99999999999999645 ) ) ;
#8704=VECTOR ( 'NONE', #1015, 1000.000000000000000 ) ;
#8708=EDGE_LOOP ( 'NONE', ( #2838, #3208, #8662, #5286 ) ) ;
#8709=CARTESIAN_POINT ( 'NONE',  ( 37.00000000000000000, -15.90990257669733943, -82.90990257669729147 ) ) ;
#8710=ORIENTED_EDGE ( 'NONE', *, *, #2836, .F. ) ;
#8716=DIRECTION ( 'NONE',  ( 0.000000000000000000, 0.000000000000000000, 1.000000000000000000 ) ) ;
#8717=MECHANICAL_DESIGN_GEOMETRIC_PRESENTATION_REPRESENTATION('',(#6579),#1046);
#8718=CARTESIAN_POINT ( 'NONE',  ( 51.96152422706632024, 29.99999999999999645, -12.99999999999999822 ) ) ;
#8719=DIRECTION ( 'NONE',  ( -1.000000000000000000, 0.000000000000000000, 0.000000000000000000 ) ) ;
#8721=ADVANCED_FACE ( 'NONE', ( #4906 ), #8602, .F. ) ;
#8723=ORIENTED_EDGE ( 'NONE', *, *, #9381, .T. ) ;
#8726=AXIS2_PLACEMENT_3D ( 'NONE', #5163, #1461, #7226 ) ;
#8731=AXIS2_PLACEMENT_3D ( 'NONE', #2892, #1588, #6599 ) ;
#8738=FACE_BOUND ( 'NONE', #9409, .T. ) ;
#8739=DIRECTION ( 'NONE',  ( -1.000000000000000000, 0.000000000000000000, 0.000000000000000000 ) ) ;
#8741=EDGE_CURVE ( 'NONE', #18, #7294, #279, .T. ) ;
#8751=VECTOR ( 'NONE', #179, 1000.000000000000000 ) ;
#8753=DIRECTION ( 'NONE',  ( -1.000000000000000000, 0.000000000000000000, 0.000000000000000000 ) ) ;
#8754=VERTEX_POINT ( 'NONE', #7839 ) ;
#8755=DIRECTION ( 'NONE',  ( -1.000000000000000000, 0.000000000000000000, -0.000000000000000000 ) ) ;
#8760=ADVANCED_FACE ( 'NONE', ( #8469 ), #570, .T. ) ;
#8764=ORIENTED_EDGE ( 'NONE', *, *, #3370, .T. ) ;
#8765=ORIENTED_EDGE ( 'NONE', *, *, #1111, .T. ) ;
#8770=FACE_OUTER_BOUND ( 'NONE', #626, .T. ) ;
#8771=AXIS2_PLACEMENT_3D ( 'NONE', #677, #2847, #8515 ) ;
#8776=ORIENTED_EDGE ( 'NONE', *, *, #5637, .T. ) ;
#8783=VERTEX_POINT ( 'NONE', #2026 ) ;
#8786=ORIENTED_EDGE ( 'NONE', *, *, #1031, .T. ) ;
#8793=FACE_OUTER_BOUND ( 'NONE', #5502, .T. ) ;
#8794=LINE ( 'NONE', #5198, #2571 ) ;
#8799=LINE ( 'NONE', #5979, #1789 ) ;
#8800=CARTESIAN_POINT ( 'NONE',  ( -53.29490495164537833, -3.673940397442057600E-15, -70.00000000000000000 ) ) ;
#8801=AXIS2_PLACEMENT_3D ( 'NONE', #3933, #6965, #6157 ) ;
#8804=ORIENTED_EDGE ( 'NONE', *, *, #3370, .F. ) ;
#8806=CARTESIAN_POINT ( 'NONE',  ( 53.29490495164537833, -27.56180520566615044, -81.40266088840111536 ) ) ;
#8807=ORIENTED_EDGE ( 'NONE', *, *, #1848, .F. ) ;
#8813=EDGE_CURVE ( 'NONE', #4316, #6932, #1883, .T. ) ;
#8815=EDGE_CURVE ( 'NONE', #6613, #6513, #7254, .T. ) ;
#8817=CYLINDRICAL_SURFACE ( 'NONE', #3380, 3.000000000000002665 ) ;
#8818=DIRECTION ( 'NONE',  ( -1.000000000000000000, -0.000000000000000000, -0.000000000000000000 ) ) ;
#8829=CARTESIAN_POINT ( 'NONE',  ( -57.72192878071319910, -19.00148731544556568, -33.94573509506513176 ) ) ;
#8831=ORIENTED_EDGE ( 'NONE', *, *, #5962, .F. ) ;
#8836=CARTESIAN_POINT ( 'NONE',  ( 19.74999999999999645, 43.00000000000000000, -25.00000000000000000 ) ) ;
#8840=DIRECTION ( 'NONE',  ( 0.000000000000000000, 0.000000000000000000, 1.000000000000000000 ) ) ;
#8850=VECTOR ( 'NONE', #6442, 1000.000000000000114 ) ;
#8851=CARTESIAN_POINT ( 'NONE',  ( -19.74999999999999645, -43.00000000000000000, 11.99999999999999645 ) ) ;
#8854=CYLINDRICAL_SURFACE ( 'NONE', #6478, 15.00000000000000000 ) ;
#8859=VERTEX_POINT ( 'NONE', #4375 ) ;
#8865=DIRECTION ( 'NONE',  ( -0.000000000000000000, -0.000000000000000000, 1.000000000000000000 ) ) ;
#8873=CIRCLE ( 'NONE', #5508, 3.000000000000002665 ) ;
#8874=CARTESIAN_POINT ( 'NONE',  ( -15.99999999999999645, -49.08300322764475254, -4.730698601353939381 ) ) ;
#8875=AXIS2_PLACEMENT_3D ( 'NONE', #445, #6456, #4095 ) ;
#8876=ORIENTED_EDGE ( 'NONE', *, *, #1615, .F. ) ;
#8878=AXIS2_PLACEMENT_3D ( 'NONE', #1369, #4490, #7417 ) ;
#8880=AXIS2_PLACEMENT_3D ( 'NONE', #3470, #5603, #5746 ) ;
#8881=FACE_OUTER_BOUND ( 'NONE', #3226, .T. ) ;
#8882=CARTESIAN_POINT ( 'NONE',  ( -60.00000000000001421, -9.637301612213116542, -29.99999999999998934 ) ) ;
#8884=VERTEX_POINT ( 'NONE', #3748 ) ;
#8886=CARTESIAN_POINT ( 'NONE',  ( -37.00000000000000711, 15.90990257669733943, -85.90990257669729147 ) ) ;
#8894=ORIENTED_EDGE ( 'NONE', *, *, #7281, .F. ) ;
#8898=LINE ( 'NONE', #3718, #2332 ) ;
#8900=ORIENTED_EDGE ( 'NONE', *, *, #8411, .F. ) ;
#8901=ORIENTED_EDGE ( 'NONE', *, *, #8520, .T. ) ;
#8910=DIRECTION ( 'NONE',  ( 0.7071067811865426878, 8.659560562354874926E-17, -0.7071067811865524577 ) ) ;
#8911=EDGE_CURVE ( 'NONE', #2503, #3864, #1965, .T. ) ;
#8912=LINE ( 'NONE', #7421, #9257 ) ;
#8916=ORIENTED_EDGE ( 'NONE', *, *, #441, .T. ) ;
#8922=EDGE_CURVE ( 'NONE', #8859, #2372, #3583, .T. ) ;
#8923=LINE ( 'NONE', #49, #9472 ) ;
#8933=ADVANCED_FACE ( 'NONE', ( #1440 ), #2889, .F. ) ;
#8951=CARTESIAN_POINT ( 'NONE',  ( -53.29490495164537833, -15.90990257669733943, -88.90990257669730568 ) ) ;
#8960=CARTESIAN_POINT ( 'NONE',  ( -37.22467645238198486, -47.05659850664388699, -0.5000000000000038858 ) ) ;
#8967=ORIENTED_EDGE ( 'NONE', *, *, #7589, .F. ) ;
#8971=CARTESIAN_POINT ( 'NONE',  ( 12.55753963192706557, 30.00000000000000000, -8.879521428754532764 ) ) ;
#8972=CARTESIAN_POINT ( 'NONE',  ( 51.96152422706632734, -30.00000000000000000, -80.85015119857384036 ) ) ;
#8985=DIRECTION ( 'NONE',  ( -0.000000000000000000, -0.000000000000000000, 1.000000000000000000 ) ) ;
#8994=AXIS2_PLACEMENT_3D ( 'NONE', #837, #2340, #1664 ) ;
#8999=ORIENTED_EDGE ( 'NONE', *, *, #258, .F. ) ;
#9000=DIRECTION ( 'NONE',  ( 0.000000000000000000, 0.000000000000000000, 1.000000000000000000 ) ) ;
#9013=ORIENTED_EDGE ( 'NONE', *, *, #844, .T. ) ;
#9017=CIRCLE ( 'NONE', #1655, 3.000000000000002665 ) ;
#9019=EDGE_LOOP ( 'NONE', ( #856, #7604, #8632, #174 ) ) ;
#9021=AXIS2_PLACEMENT_3D ( 'NONE', #1908, #6429, #9346 ) ;
#9022=CARTESIAN_POINT ( 'NONE',  ( 60.00000000000000000, 15.90990257669733943, -51.09009742330271564 ) ) ;
#9026=EDGE_CURVE ( 'NONE', #8783, #2826, #1826, .T. ) ;
#9033=EDGE_CURVE ( 'NONE', #472, #1938, #7690, .T. ) ;
#9044=ORIENTED_EDGE ( 'NONE', *, *, #8052, .T. ) ;
#9046=ORIENTED_EDGE ( 'NONE', *, *, #8520, .F. ) ;
#9049=CARTESIAN_POINT ( 'NONE',  ( 60.00000000000000000, -15.90990257669733943, -54.09009742330271564 ) ) ;
#9054=ADVANCED_FACE ( 'NONE', ( #3265 ), #4711, .F. ) ;
#9055=CARTESIAN_POINT ( 'NONE',  ( 39.50000000000000000, -30.00000000000000355, -82.50000000000001421 ) ) ;
#9056=EDGE_CURVE ( 'NONE', #4256, #804, #6601, .T. ) ;
#9057=DIRECTION ( 'NONE',  ( -1.000000000000000000, 0.000000000000000000, -0.000000000000000000 ) ) ;
#9061=DIRECTION ( 'NONE',  ( -0.8660254037844399289, 0.000000000000000000, -0.4999999999999977240 ) ) ;
#9065=DIRECTION ( 'NONE',  ( -1.000000000000000000, -0.000000000000000000, -0.000000000000000000 ) ) ;
#9069=LINE ( 'NONE', #1682, #416 ) ;
#9070=EDGE_CURVE ( 'NONE', #4478, #1970, #6416, .T. ) ;
#9072=EDGE_LOOP ( 'NONE', ( #1366, #8283 ) ) ;
#9080=ORIENTED_EDGE ( 'NONE', *, *, #753, .F. ) ;
#9081=ORIENTED_EDGE ( 'NONE', *, *, #3408, .F. ) ;
#9085=CARTESIAN_POINT ( 'NONE',  ( -53.29490495164537833, 18.67545040036925386, -90.28901569369799063 ) ) ;
#9087=ORIENTED_EDGE ( 'NONE', *, *, #6134, .F. ) ;
#9089=ORIENTED_EDGE ( 'NONE', *, *, #5679, .T. ) ;
#9092=CARTESIAN_POINT ( 'NONE',  ( 53.29490495164537833, -27.56180520566615044, -41.61356529332876875 ) ) ;
#9093=DIRECTION ( 'NONE',  ( -0.6785983445458488861, -0.2810846377148297770, -0.6785983445458412255 ) ) ;
#9095=DIRECTION ( 'NONE',  ( -0.000000000000000000, -0.000000000000000000, -1.000000000000000000 ) ) ;
#9096=DIRECTION ( 'NONE',  ( -1.000000000000000000, 0.000000000000000000, 0.000000000000000000 ) ) ;
#9097=CYLINDRICAL_SURFACE ( 'NONE', #520, 3.000000000000002665 ) ;
#9100=ORIENTED_EDGE ( 'NONE', *, *, #7940, .F. ) ;
#9101=EDGE_CURVE ( 'NONE', #2523, #4781, #2269, .T. ) ;
#9103=CARTESIAN_POINT ( 'NONE',  ( 34.25000000000000000, 43.00000000000000000, -25.00000000000000000 ) ) ;
#9108=ADVANCED_FACE ( 'NONE', ( #2464 ), #6882, .F. ) ;
#9110=EDGE_LOOP ( 'NONE', ( #7791, #5047, #624, #216, #3167, #9080 ) ) ;
#9111=VECTOR ( 'NONE', #6481, 1000.000000000000000 ) ;
#9112=CARTESIAN_POINT ( 'NONE',  ( 50.79490495164537833, -30.00000000000000355, -82.50000000000001421 ) ) ;
#9113=DIRECTION ( 'NONE',  ( -0.000000000000000000, -0.000000000000000000, -1.000000000000000000 ) ) ;
#9118=EDGE_CURVE ( 'NONE', #7922, #4458, #5953, .T. ) ;
#9125=CARTESIAN_POINT ( 'NONE',  ( 37.00000000000000000, -21.98223304703364889, -86.98223304703364533 ) ) ;
#9126=ORIENTED_EDGE ( 'NONE', *, *, #7958, .F. ) ;
#9127=LINE ( 'NONE', #3590, #5649 ) ;
#9129=CARTESIAN_POINT ( 'NONE',  ( 51.96152422706632734, 30.00000000000000000, -134.0000000000000284 ) ) ;
#9131=LINE ( 'NONE', #2802, #4395 ) ;
#9136=ORIENTED_EDGE ( 'NONE', *, *, #3603, .T. ) ;
#9140=DIRECTION ( 'NONE',  ( -0.6785983445458478869, 0.2810846377148137898, 0.6785983445458488861 ) ) ;
#9141=VECTOR ( 'NONE', #3629, 1000.000000000000000 ) ;
#9142=AXIS2_PLACEMENT_3D ( 'NONE', #1316, #551, #5025 ) ;
#9146=EDGE_LOOP ( 'NONE', ( #7558, #1744, #440, #4982 ) ) ;
#9155=DIRECTION ( 'NONE',  ( -1.000000000000000000, 0.000000000000000000, 0.000000000000000000 ) ) ;
#9159=CARTESIAN_POINT ( 'NONE',  ( 53.29490495164537833, -27.56180520566615044, -81.40266088840111536 ) ) ;
#9161=AXIS2_PLACEMENT_3D ( 'NONE', #2968, #9155, #467 ) ;
#9163=ORIENTED_EDGE ( 'NONE', *, *, #9026, .F. ) ;
#9167=( BOUNDED_CURVE ( )  B_SPLINE_CURVE ( 3, ( #5456, #979, #3914, #9092 ),
 .UNSPECIFIED., .F., .F. ) 
 B_SPLINE_CURVE_WITH_KNOTS ( ( 4, 4 ),
 ( 0.000000000000000000, 0.4772783968222097384 ),
 .UNSPECIFIED. ) 
 CURVE ( )  GEOMETRIC_REPRESENTATION_ITEM ( )  RATIONAL_B_SPLINE_CURVE ( ( 1.000000000000000000, 0.9811070276743185659, 0.9811070276743185659, 1.000000000000000000 ) ) 
 REPRESENTATION_ITEM ( '' )  );
#9171=FACE_OUTER_BOUND ( 'NONE', #3037, .T. ) ;
#9175=FACE_OUTER_BOUND ( 'NONE', #3818, .T. ) ;
#9179=VECTOR ( 'NONE', #7160, 1000.000000000000000 ) ;
#9183=CYLINDRICAL_SURFACE ( 'NONE', #5975, 3.000000000000002665 ) ;
#9184=DIRECTION ( 'NONE',  ( -1.000000000000000000, 0.000000000000000000, 0.000000000000000000 ) ) ;
#9188=ORIENTED_EDGE ( 'NONE', *, *, #4596, .T. ) ;
#9191=CARTESIAN_POINT ( 'NONE',  ( 37.00000000000000000, 15.90990257669733943, -54.09009742330271564 ) ) ;
#9192=CARTESIAN_POINT ( 'NONE',  ( -51.96152422706631313, 30.00000000000000711, -12.99999999999999289 ) ) ;
#9195=ORIENTED_EDGE ( 'NONE', *, *, #1517, .T. ) ;
#9199=ORIENTED_EDGE ( 'NONE', *, *, #1341, .T. ) ;
#9205=ORIENTED_EDGE ( 'NONE', *, *, #5243, .F. ) ;
#9210=CARTESIAN_POINT ( 'NONE',  ( 53.29490495164537833, -15.90990257669733943, -85.90990257669729147 ) ) ;
#9212=DIRECTION ( 'NONE',  ( 0.6785983445458459995, 0.2810846377148253916, -0.6785983445458459995 ) ) ;
#9214=ORIENTED_EDGE ( 'NONE', *, *, #8815, .T. ) ;
#9215=ORIENTED_EDGE ( 'NONE', *, *, #553, .F. ) ;
#9224=CYLINDRICAL_SURFACE ( 'NONE', #8875, 11.00000000000000711 ) ;
#9225=CARTESIAN_POINT ( 'NONE',  ( -37.22467645238203460, -47.05659850664382304, -5.608807313787673721 ) ) ;
#9226=CARTESIAN_POINT ( 'NONE',  ( -60.00000000000000000, 60.00000000000000000, 0.000000000000000000 ) ) ;
#9228=ORIENTED_EDGE ( 'NONE', *, *, #6271, .T. ) ;
#9231=EDGE_CURVE ( 'NONE', #955, #6124, #4729, .T. ) ;
#9235=ADVANCED_FACE ( 'NONE', ( #1859 ), #5325, .F. ) ;
#9242=DIRECTION ( 'NONE',  ( 1.000000000000000000, 0.000000000000000000, 0.000000000000000000 ) ) ;
#9243=ORIENTED_EDGE ( 'NONE', *, *, #7231, .F. ) ;
#9249=DIRECTION ( 'NONE',  ( -1.000000000000000000, 0.000000000000000000, 0.000000000000000000 ) ) ;
#9254=EDGE_CURVE ( 'NONE', #5515, #1435, #4024, .T. ) ;
#9256=DIRECTION ( 'NONE',  ( 0.000000000000000000, 0.000000000000000000, -1.000000000000000000 ) ) ;
#9257=VECTOR ( 'NONE', #5272, 1000.000000000000000 ) ;
#9265=CARTESIAN_POINT ( 'NONE',  ( 41.99999999999997868, -12.50000000000000355, -100.0000000000000000 ) ) ;
#9275=ORIENTED_EDGE ( 'NONE', *, *, #368, .T. ) ;
#9280=EDGE_CURVE ( 'NONE', #4271, #6932, #6046, .T. ) ;
#9286=ORIENTED_EDGE ( 'NONE', *, *, #7344, .F. ) ;
#9290=CARTESIAN_POINT ( 'NONE',  ( -19.74999999999999645, 43.00000000000000000, -25.00000000000000000 ) ) ;
#9291=DIRECTION ( 'NONE',  ( 0.000000000000000000, 0.000000000000000000, -1.000000000000000000 ) ) ;
#9292=DIRECTION ( 'NONE',  ( -0.5773502691896249539, -0.5773502691896263972, 0.5773502691896258421 ) ) ;
#9295=CARTESIAN_POINT ( 'NONE',  ( -37.73845885098648978, 45.76160744848121453, -6.169970105658134862 ) ) ;
#9297=EDGE_LOOP ( 'NONE', ( #5586, #8096, #5070, #5860 ) ) ;
#9302=FACE_OUTER_BOUND ( 'NONE', #8056, .T. ) ;
#9312=ADVANCED_FACE ( 'NONE', ( #945 ), #4789, .F. ) ;
#9317=CARTESIAN_POINT ( 'NONE',  ( 37.00000000000000000, -3.673940397442057600E-15, -70.00000000000000000 ) ) ;
#9324=AXIS2_PLACEMENT_3D ( 'NONE', #4165, #3531, #7090 ) ;
#9326=ORIENTED_EDGE ( 'NONE', *, *, #3548, .F. ) ;
#9329=DIRECTION ( 'NONE',  ( 0.000000000000000000, 1.000000000000000000, 0.000000000000000000 ) ) ;
#9330=ADVANCED_FACE ( 'NONE', ( #6812 ), #4068, .T. ) ;
#9335=CARTESIAN_POINT ( 'NONE',  ( 60.00000000000000000, 7.347880794884118356E-15, 25.00000000000000000 ) ) ;
#9339=EDGE_CURVE ( 'NONE', #8518, #55, #4254, .T. ) ;
#9343=EDGE_CURVE ( 'NONE', #7585, #3888, #7204, .T. ) ;
#9345=EDGE_CURVE ( 'NONE', #1435, #6513, #8687, .T. ) ;
#9346=DIRECTION ( 'NONE',  ( 1.000000000000000000, 0.000000000000000000, 0.000000000000000000 ) ) ;
#9347=FACE_OUTER_BOUND ( 'NONE', #183, .T. ) ;
#9358=ADVANCED_FACE ( 'NONE', ( #7132 ), #5565, .F. ) ;
#9359=CARTESIAN_POINT ( 'NONE',  ( 60.00000000000000000, 7.347880794884118356E-15, -30.00000000000000000 ) ) ;
#9365=EDGE_LOOP ( 'NONE', ( #8114, #3991 ) ) ;
#9377=ORIENTED_EDGE ( 'NONE', *, *, #6654, .T. ) ;
#9381=EDGE_CURVE ( 'NONE', #2690, #1211, #4202, .T. ) ;
#9382=CARTESIAN_POINT ( 'NONE',  ( 37.73845885098648978, 45.76160744848121453, -6.169970105658139303 ) ) ;
#9383=DIRECTION ( 'NONE',  ( 0.5773502691896252870, 0.5773502691896258421, 0.5773502691896261751 ) ) ;
#9388=DIRECTION ( 'NONE',  ( 1.000000000000000000, 0.000000000000000000, 0.000000000000000000 ) ) ;
#9390=ORIENTED_EDGE ( 'NONE', *, *, #7764, .F. ) ;
#9393=DIRECTION ( 'NONE',  ( 1.000000000000000000, 0.000000000000000000, 0.000000000000000000 ) ) ;
#9395=AXIS2_PLACEMENT_3D ( 'NONE', #6076, #3228, #6891 ) ;
#9396=EDGE_CURVE ( 'NONE', #8464, #287, #8670, .T. ) ;
#9404=DIRECTION ( 'NONE',  ( 0.000000000000000000, 0.7071067811865477948, -0.7071067811865473507 ) ) ;
#9409=EDGE_LOOP ( 'NONE', ( #7201, #5983 ) ) ;
#9410=VECTOR ( 'NONE', #8619, 1000.000000000000000 ) ;
#9416=DIRECTION ( 'NONE',  ( -1.000000000000000000, 0.000000000000000000, 0.000000000000000000 ) ) ;
#9417=CARTESIAN_POINT ( 'NONE',  ( 53.29490495164537833, 27.56180520566615044, -81.40266088840108694 ) ) ;
#9418=CARTESIAN_POINT ( 'NONE',  ( 27.00000000000000000, -43.00000000000000000, 11.99999999999999645 ) ) ;
#9423=ORIENTED_EDGE ( 'NONE', *, *, #4886, .F. ) ;
#9424=DIRECTION ( 'NONE',  ( 0.000000000000000000, 0.000000000000000000, -1.000000000000000000 ) ) ;
#9425=VECTOR ( 'NONE', #6420, 1000.000000000000000 ) ;
#9426=VERTEX_POINT ( 'NONE', #7224 ) ;
#9429=CARTESIAN_POINT ( 'NONE',  ( 28.61406079152380144, 10.49089634068024068, -86.61406079152378368 ) ) ;
#9430=CARTESIAN_POINT ( 'NONE',  ( 37.22467645238199196, 47.05659850664387278, -5.608807313787652404 ) ) ;
#9438=CARTESIAN_POINT ( 'NONE',  ( -37.00000000000000000, -30.00000000000000000, -95.00000000000000000 ) ) ;
#9443=DIRECTION ( 'NONE',  ( -1.000000000000000000, 0.000000000000000000, 0.000000000000000000 ) ) ;
#9446=EDGE_LOOP ( 'NONE', ( #7078, #7133 ) ) ;
#9449=LINE ( 'NONE', #3549, #881 ) ;
#9455=ORIENTED_EDGE ( 'NONE', *, *, #2941, .F. ) ;
#9456=ORIENTED_EDGE ( 'NONE', *, *, #1554, .F. ) ;
#9462=LINE ( 'NONE', #98, #1311 ) ;
#9465=CARTESIAN_POINT ( 'NONE',  ( 53.29490495164537833, -11.46446609406722850, -97.50000000000002842 ) ) ;
#9467=CARTESIAN_POINT ( 'NONE',  ( -15.99999999999999645, 43.00000000000000000, -7.366666666666667140 ) ) ;
#9468=AXIS2_PLACEMENT_3D ( 'NONE', #7551, #4523, #5353 ) ;
#9472=VECTOR ( 'NONE', #3068, 1000.000000000000000 ) ;
#9509=COLOUR_RGB('Light Blue',0.38,0.62,0.78);
#9510=FILL_AREA_STYLE_COLOUR('',#9509);
#9511=FILL_AREA_STYLE('',(#9510));
#9512=SURFACE_STYLE_FILL_AREA(#9511);
#9513=SURFACE_SIDE_STYLE('',(#9512));
#9514=SURFACE_STYLE_USAGE(.BOTH.,#9513);
#9515=PRESENTATION_STYLE_ASSIGNMENT((#9514));
ENDSEC;
END-ISO-10303-21;
